ISO-10303-21;
HEADER;
FILE_DESCRIPTION (('STEP AP214'),
    '1' );
FILE_NAME ('pad arm right_right.step',
    '2026-10-08T07:58:12',
    ( '' ),
    ( '' ),
    'SwSTEP 2.0',
    'SolidWorks 2026',
    '' );
FILE_SCHEMA (( 'AUTOMOTIVE_DESIGN' ));
ENDSEC;

DATA;
#12=SURFACE_SIDE_STYLE ('',( #18233 ) ) ;
#16=DIRECTION ( 'NONE',  ( 1.000000000000000000, 0.000000000000000000, 0.000000000000000000 ) ) ;
#57=DIRECTION ( 'NONE',  ( 0.000000000000000000, -1.000000000000000000, 0.000000000000000000 ) ) ;
#59=DIRECTION ( 'NONE',  ( -0.000000000000000000, -0.000000000000000000, -1.000000000000000000 ) ) ;
#69=CARTESIAN_POINT ( 'NONE',  ( -59.30520453566667527, 194.9296309105606326, -2.372451168785852715 ) ) ;
#112=CARTESIAN_POINT ( 'NONE',  ( -67.50001199999999812, 168.5168296348864203, 10.36982646209945891 ) ) ;
#127=UNCERTAINTY_MEASURE_WITH_UNIT (LENGTH_MEASURE( 1.000000000000000082E-05 ), #13064, 'distance_accuracy_value', 'NONE');
#142=CARTESIAN_POINT ( 'NONE',  ( -58.50000000000001421, -88.00000000000000000, -20.00000000000000000 ) ) ;
#143=CARTESIAN_POINT ( 'NONE',  ( 0.000000000000000000, 0.000000000000000000, -20.00000000000000000 ) ) ;
#157=EDGE_CURVE ( 'NONE', #28109, #32153, #10692, .T. ) ;
#161=VERTEX_POINT ( 'NONE', #19672 ) ;
#162=ORIENTED_EDGE ( 'NONE', *, *, #20206, .F. ) ;
#199=EDGE_LOOP ( 'NONE', ( #6046, #19847, #15492, #25201, #18551, #25086 ) ) ;
#213=EDGE_CURVE ( 'NONE', #19514, #25076, #28012, .T. ) ;
#240=CARTESIAN_POINT ( 'NONE',  ( -60.15146012614710003, 194.9557722165940845, -1.884122726181822971 ) ) ;
#273=DIRECTION ( 'NONE',  ( 0.000000000000000000, 0.000000000000000000, -1.000000000000000000 ) ) ;
#279=CARTESIAN_POINT ( 'NONE',  ( -67.50001199999999812, 171.4562830276601630, 4.407803664655115305 ) ) ;
#329=DIRECTION ( 'NONE',  ( 0.000000000000000000, 1.000000000000000000, 0.000000000000000000 ) ) ;
#341=CARTESIAN_POINT ( 'NONE',  ( -58.50000000000002132, 194.9217985566782829, 2.500000000000000000 ) ) ;
#452=SURFACE_SIDE_STYLE ('',( #29228 ) ) ;
#465=DIRECTION ( 'NONE',  ( 0.000000000000000000, 0.000000000000000000, -1.000000000000000000 ) ) ;
#488=CARTESIAN_POINT ( 'NONE',  ( -52.50000000000002132, 155.0000000000000000, 6.938893903907228378E-15 ) ) ;
#610=VERTEX_POINT ( 'NONE', #8008 ) ;
#623=CARTESIAN_POINT ( 'NONE',  ( -125.0000000000000000, 0.000000000000000000, 20.00000000000000000 ) ) ;
#646=( BOUNDED_CURVE ( )  B_SPLINE_CURVE ( 3, ( #7649, #10206, #20750, #10043 ),
 .UNSPECIFIED., .F., .T. ) 
 B_SPLINE_CURVE_WITH_KNOTS ( ( 4, 4 ),
 ( 0.000000000000000000, 0.5248789335016748048 ),
 .UNSPECIFIED. ) 
 CURVE ( )  GEOMETRIC_REPRESENTATION_ITEM ( )  RATIONAL_B_SPLINE_CURVE ( ( 1.000000000000000000, 0.9771733092046011038, 0.9771733092046011038, 1.000000000000000000 ) ) 
 REPRESENTATION_ITEM ( '' )  );
#651=AXIS2_PLACEMENT_3D ( 'NONE', #1417, #30036, #33096 ) ;
#718=DIRECTION ( 'NONE',  ( 0.000000000000000000, 0.000000000000000000, -1.000000000000000000 ) ) ;
#737=CARTESIAN_POINT ( 'NONE',  ( -58.50000000000002132, 209.9999999999999716, 0.000000000000000000 ) ) ;
#747=VERTEX_POINT ( 'NONE', #26712 ) ;
#774=CARTESIAN_POINT ( 'NONE',  ( -67.50000599999999906, 155.0000000000000000, -17.00000000000000711 ) ) ;
#778=ORIENTED_EDGE ( 'NONE', *, *, #23557, .F. ) ;
#816=DIRECTION ( 'NONE',  ( -1.000000000000000000, -0.000000000000000000, 0.000000000000000000 ) ) ;
#894=CARTESIAN_POINT ( 'NONE',  ( -67.50000000000000000, -92.00000000000000000, 17.00000000000001421 ) ) ;
#897=DIRECTION ( 'NONE',  ( 0.000000000000000000, -1.000000000000000000, 0.000000000000000000 ) ) ;
#936=CARTESIAN_POINT ( 'NONE',  ( -67.50001199999998391, 160.4776661921571588, -16.13174377802661752 ) ) ;
#982=VERTEX_POINT ( 'NONE', #25338 ) ;
#1028=EDGE_CURVE ( 'NONE', #8086, #25683, #17164, .T. ) ;
#1035=ORIENTED_EDGE ( 'NONE', *, *, #13146, .F. ) ;
#1055=ADVANCED_FACE ( 'NONE', ( #7461 ), #15286, .F. ) ;
#1067=DIRECTION ( 'NONE',  ( 0.5773502691896268413, -0.5773502691896268413, -0.5773502691896235106 ) ) ;
#1081=VERTEX_POINT ( 'NONE', #33517 ) ;
#1094=ADVANCED_BREP_SHAPE_REPRESENTATION ( '', ( #23982, #2404 ), #31228 ) ;
#1115=LINE ( 'NONE', #21550, #33373 ) ;
#1242=ORIENTED_EDGE ( 'NONE', *, *, #12526, .T. ) ;
#1244=ADVANCED_FACE ( 'NONE', ( #29075, #31630 ), #29240, .T. ) ;
#1313=AXIS2_PLACEMENT_3D ( 'NONE', #10723, #17889, #4937 ) ;
#1386=CARTESIAN_POINT ( 'NONE',  ( -56.33087447058203168, 194.9805812333615620, -1.253637678855320958 ) ) ;
#1401=CARTESIAN_POINT ( 'NONE',  ( -64.50000000000000000, 120.3589838486224437, 20.00000000000000000 ) ) ;
#1417=CARTESIAN_POINT ( 'NONE',  ( -58.50000000000002132, 209.9999999999999716, 0.000000000000000000 ) ) ;
#1455=ORIENTED_EDGE ( 'NONE', *, *, #14682, .F. ) ;
#1460=CIRCLE ( 'NONE', #25958, 40.00000000000000711 ) ;
#1598=CARTESIAN_POINT ( 'NONE',  ( -60.00000000000000000, -7.347880794884118356E-15, 270.4495957273638282 ) ) ;
#1601=ORIENTED_EDGE ( 'NONE', *, *, #18063, .F. ) ;
#1684=CARTESIAN_POINT ( 'NONE',  ( -52.50000000000002132, 0.000000000000000000, -20.00000000000000000 ) ) ;
#1695=VERTEX_POINT ( 'NONE', #5196 ) ;
#1697=ORIENTED_EDGE ( 'NONE', *, *, #213, .F. ) ;
#1699=FACE_BOUND ( 'NONE', #15661, .T. ) ;
#1716=CARTESIAN_POINT ( 'NONE',  ( -56.01643337169826964, 194.9989636249862599, -0.3293050612182487069 ) ) ;
#1717=CARTESIAN_POINT ( 'NONE',  ( -68.50000000000000000, 215.0000000000000000, 0.000000000000000000 ) ) ;
#1737=DIRECTION ( 'NONE',  ( -0.000000000000000000, -0.000000000000000000, -1.000000000000000000 ) ) ;
#1741=FACE_OUTER_BOUND ( 'NONE', #4713, .T. ) ;
#1829=CARTESIAN_POINT ( 'NONE',  ( -64.50000000000000000, 120.3589838486224579, -20.00000000000000000 ) ) ;
#1894=CARTESIAN_POINT ( 'NONE',  ( -58.17468396801123731, 194.9227987135369062, -2.484183799773476142 ) ) ;
#1903=DIRECTION ( 'NONE',  ( 0.000000000000000000, 2.081668171172168119E-15, -1.000000000000000000 ) ) ;
#2083=CIRCLE ( 'NONE', #24369, 2.500000000000000000 ) ;
#2123=CARTESIAN_POINT ( 'NONE',  ( -59.75427847806285797, 194.9412682558892982, -2.168710897896606760 ) ) ;
#2214=CARTESIAN_POINT ( 'NONE',  ( -63.49999999999884892, 215.0000000000003979, 0.000000000000000000 ) ) ;
#2235=FACE_OUTER_BOUND ( 'NONE', #16029, .T. ) ;
#2257=LINE ( 'NONE', #30198, #15419 ) ;
#2270=CARTESIAN_POINT ( 'NONE',  ( -67.50000599999999906, 155.0000000000000000, 17.00000000000001421 ) ) ;
#2330=LINE ( 'NONE', #20551, #4129 ) ;
#2332=CARTESIAN_POINT ( 'NONE',  ( -67.50001199999999812, 160.4776661921571588, 16.13174377802662462 ) ) ;
#2337=ORIENTED_EDGE ( 'NONE', *, *, #6806, .F. ) ;
#2349=DIRECTION ( 'NONE',  ( -0.000000000000000000, -0.000000000000000000, -1.000000000000000000 ) ) ;
#2380=DIRECTION ( 'NONE',  ( -0.000000000000000000, -0.000000000000000000, -1.000000000000000000 ) ) ;
#2404=AXIS2_PLACEMENT_3D ( 'NONE', #8872, #11941, #4266 ) ;
#2428=VERTEX_POINT ( 'NONE', #7346 ) ;
#2448=FACE_OUTER_BOUND ( 'NONE', #29818, .T. ) ;
#2458=CARTESIAN_POINT ( 'NONE',  ( -59.14934243545564385, 194.9267577168561161, -2.419719764051426747 ) ) ;
#2461=EDGE_CURVE ( 'NONE', #33083, #6207, #11942, .T. ) ;
#2534=FACE_OUTER_BOUND ( 'NONE', #31931, .T. ) ;
#2564=CARTESIAN_POINT ( 'NONE',  ( -58.50000000000002132, 209.9999999999999716, 2.500000000000000000 ) ) ;
#2613=CARTESIAN_POINT ( 'NONE',  ( -67.50001199999996970, 138.8682562219733541, -5.477666192157146341 ) ) ;
#2677=CARTESIAN_POINT ( 'NONE',  ( -67.50001199999998391, 159.4078036646551197, 16.45628302766014528 ) ) ;
#2688=EDGE_LOOP ( 'NONE', ( #32080, #32577, #29359, #16102 ) ) ;
#2731=DIRECTION ( 'NONE',  ( 0.000000000000000000, 0.000000000000000000, 1.000000000000000000 ) ) ;
#2794=CARTESIAN_POINT ( 'NONE',  ( -60.87270596256635713, 194.9921970430798979, -0.8044259506661830539 ) ) ;
#2875=EDGE_CURVE ( 'NONE', #27919, #25683, #11398, .T. ) ;
#3035=( BOUNDED_CURVE ( )  B_SPLINE_CURVE ( 3, ( #15301, #5081, #30646, #23476 ),
 .UNSPECIFIED., .F., .T. ) 
 B_SPLINE_CURVE_WITH_KNOTS ( ( 4, 4 ),
 ( 5.758306373677911871, 6.283185307179586232 ),
 .UNSPECIFIED. ) 
 CURVE ( )  GEOMETRIC_REPRESENTATION_ITEM ( )  RATIONAL_B_SPLINE_CURVE ( ( 1.000000000000000000, 0.9771733092046011038, 0.9771733092046011038, 1.000000000000000000 ) ) 
 REPRESENTATION_ITEM ( '' )  );
#3058=PRODUCT_CONTEXT ( 'NONE', #7246, 'mechanical' ) ;
#3116=( GEOMETRIC_REPRESENTATION_CONTEXT ( 3 ) GLOBAL_UNCERTAINTY_ASSIGNED_CONTEXT ( ( #127 ) ) GLOBAL_UNIT_ASSIGNED_CONTEXT ( ( #13064, #26667, #19009 ) ) REPRESENTATION_CONTEXT ( 'NONE', 'WORKASPACE' ) );
#3137=CARTESIAN_POINT ( 'NONE',  ( -52.50000000000002132, 155.0000000000000000, -16.99999999999999645 ) ) ;
#3161=CARTESIAN_POINT ( 'NONE',  ( -67.50001199999999812, 157.2252672838932597, -16.89041650604970357 ) ) ;
#3165=CIRCLE ( 'NONE', #23308, 2.500000000000000000 ) ;
#3217=ORIENTED_EDGE ( 'NONE', *, *, #28326, .T. ) ;
#3236=DIRECTION ( 'NONE',  ( 0.000000000000000000, 0.000000000000000000, 1.000000000000000000 ) ) ;
#3257=DIRECTION ( 'NONE',  ( 0.000000000000000000, 0.000000000000000000, 1.000000000000000000 ) ) ;
#3292=ORIENTED_EDGE ( 'NONE', *, *, #16187, .T. ) ;
#3333=EDGE_LOOP ( 'NONE', ( #162, #13018, #29872, #22354, #4251, #17416 ) ) ;
#3377=VERTEX_POINT ( 'NONE', #10037 ) ;
#3662=ORIENTED_EDGE ( 'NONE', *, *, #2875, .T. ) ;
#3716=AXIS2_PLACEMENT_3D ( 'NONE', #23498, #2731, #10399 ) ;
#3792=CARTESIAN_POINT ( 'NONE',  ( -65.50384660342780307, 120.9385549553365706, 18.99615339657220758 ) ) ;
#3809=DIRECTION ( 'NONE',  ( 0.000000000000000000, 0.000000000000000000, 1.000000000000000000 ) ) ;
#3813=CARTESIAN_POINT ( 'NONE',  ( -125.0000000000000000, -95.00000000000000000, -20.00000000000000000 ) ) ;
#3833=CARTESIAN_POINT ( 'NONE',  ( -67.50000599999999906, 155.0000000000000000, -17.00000000000000711 ) ) ;
#3883=FACE_OUTER_BOUND ( 'NONE', #31828, .T. ) ;
#3887=DIRECTION ( 'NONE',  ( -0.5773502691896268413, 0.5773502691896268413, -0.5773502691896235106 ) ) ;
#3897=DIRECTION ( 'NONE',  ( 1.000000000000000000, 0.000000000000000000, 0.000000000000000000 ) ) ;
#3908=CARTESIAN_POINT ( 'NONE',  ( -64.50000000000000000, 2.605762844159070557, 20.00000000000000000 ) ) ;
#3945=CARTESIAN_POINT ( 'NONE',  ( -64.50000000000000000, -2.605762844159085212, -20.00000000000000000 ) ) ;
#3963=EDGE_CURVE ( 'NONE', #23163, #18293, #22550, .T. ) ;
#3968=ORIENTED_EDGE ( 'NONE', *, *, #33516, .F. ) ;
#4129=VECTOR ( 'NONE', #25492, 1000.000000000000000 ) ;
#4145=DIRECTION ( 'NONE',  ( -1.000000000000000000, 0.000000000000000000, 0.000000000000000000 ) ) ;
#4202=ORIENTED_EDGE ( 'NONE', *, *, #21802, .F. ) ;
#4233=LINE ( 'NONE', #29969, #18431 ) ;
#4251=ORIENTED_EDGE ( 'NONE', *, *, #29982, .F. ) ;
#4266=DIRECTION ( 'NONE',  ( 1.000000000000000000, 0.000000000000000000, 0.000000000000000000 ) ) ;
#4323=EDGE_CURVE ( 'NONE', #24997, #747, #21840, .T. ) ;
#4444=CARTESIAN_POINT ( 'NONE',  ( -56.01598787314604522, 194.9989914758641305, 0.3258944654411097264 ) ) ;
#4451=CARTESIAN_POINT ( 'NONE',  ( -52.50000000000002132, 120.3589838486224579, -20.00000000000000000 ) ) ;
#4464=ORIENTED_EDGE ( 'NONE', *, *, #14579, .T. ) ;
#4506=CARTESIAN_POINT ( 'NONE',  ( -67.50000000000000000, 155.0000000000000000, 6.938893903907228378E-15 ) ) ;
#4558=EDGE_CURVE ( 'NONE', #4641, #16283, #10980, .T. ) ;
#4587=CARTESIAN_POINT ( 'NONE',  ( -58.50000000000002132, 185.0000000000000000, 2.500000000000000000 ) ) ;
#4638=ORIENTED_EDGE ( 'NONE', *, *, #25487, .F. ) ;
#4641=VERTEX_POINT ( 'NONE', #19784 ) ;
#4669=CARTESIAN_POINT ( 'NONE',  ( -60.02418147676856108, 194.9506531851598936, 1.988357156115594826 ) ) ;
#4678=CARTESIAN_POINT ( 'NONE',  ( -64.50000000000000000, -95.00000000000000000, 270.4495957273638282 ) ) ;
#4713=EDGE_LOOP ( 'NONE', ( #11471, #33174, #26340, #14353, #27131 ) ) ;
#4820=CARTESIAN_POINT ( 'NONE',  ( -67.50001199999998391, 139.7198396726428768, 7.533570508255921006 ) ) ;
#4838=CARTESIAN_POINT ( 'NONE',  ( -58.50000000000002132, 194.9217985566782829, 2.500000000000000000 ) ) ;
#4884=DIRECTION ( 'NONE',  ( 1.000000000000000000, 0.000000000000000000, 0.000000000000000000 ) ) ;
#4937=DIRECTION ( 'NONE',  ( 1.000000000000000000, 0.000000000000000000, 0.000000000000000000 ) ) ;
#4958=CARTESIAN_POINT ( 'NONE',  ( -57.39039945611308013, 194.9369330859559284, 2.246172506675526481 ) ) ;
#4994=CARTESIAN_POINT ( 'NONE',  ( -67.50001199999998391, 149.5223338078428696, 16.13174377802662818 ) ) ;
#5006=CARTESIAN_POINT ( 'NONE',  ( -60.38481630464774241, 194.9660974499433053, -1.650668498912690740 ) ) ;
#5053=CARTESIAN_POINT ( 'NONE',  ( -67.50001199999998391, 171.9999999999999716, -1.112647398146377142 ) ) ;
#5060=ORIENTED_EDGE ( 'NONE', *, *, #7734, .T. ) ;
#5063=ORIENTED_EDGE ( 'NONE', *, *, #19325, .T. ) ;
#5081=CARTESIAN_POINT ( 'NONE',  ( -64.96121601855533356, 1.809269760319432319, 19.53878398144468775 ) ) ;
#5107=AXIS2_PLACEMENT_3D ( 'NONE', #18569, #26226, #16 ) ;
#5125=CARTESIAN_POINT ( 'NONE',  ( -56.51026148866456111, 194.9712507328865740, 1.522362431316129916 ) ) ;
#5149=ADVANCED_FACE ( 'NONE', ( #2235 ), #12619, .T. ) ;
#5196=CARTESIAN_POINT ( 'NONE',  ( -67.50000000000000000, -92.00000000000000000, -17.00000000000001421 ) ) ;
#5323=CARTESIAN_POINT ( 'NONE',  ( -67.50001199999999812, 147.4664294917440373, 15.28016032735713559 ) ) ;
#5331=CARTESIAN_POINT ( 'NONE',  ( -64.50000000000000000, 2.605762844159070557, -20.00000000000000000 ) ) ;
#5356=ORIENTED_EDGE ( 'NONE', *, *, #20206, .T. ) ;
#5387=CARTESIAN_POINT ( 'NONE',  ( -67.50001199999999812, 156.1126473981464073, 17.00000000000001066 ) ) ;
#5390=AXIS2_PLACEMENT_3D ( 'NONE', #24568, #273, #32394 ) ;
#5477=DIRECTION ( 'NONE',  ( -1.000000000000000000, 0.000000000000000000, 0.000000000000000000 ) ) ;
#5557=CARTESIAN_POINT ( 'NONE',  ( -64.50000000000000000, 120.3589838486224437, 20.00000000000000000 ) ) ;
#5576=DIRECTION ( 'NONE',  ( 0.000000000000000000, 0.000000000000000000, -1.000000000000000000 ) ) ;
#5629=CARTESIAN_POINT ( 'NONE',  ( -63.50000000000001421, 210.0000000000000000, 0.000000000000000000 ) ) ;
#5635=CARTESIAN_POINT ( 'NONE',  ( -68.50000000000000000, 215.0000000000000000, 0.000000000000000000 ) ) ;
#5643=CIRCLE ( 'NONE', #15449, 2.500000000000000000 ) ;
#5690=DIRECTION ( 'NONE',  ( 0.000000000000000000, 0.000000000000000000, 1.000000000000000000 ) ) ;
#5695=CARTESIAN_POINT ( 'NONE',  ( -125.0000000000000000, -95.00000000000000000, 270.4495957273638282 ) ) ;
#5703=LINE ( 'NONE', #16091, #28231 ) ;
#5706=ORIENTED_EDGE ( 'NONE', *, *, #3963, .F. ) ;
#5717=SURFACE_STYLE_USAGE ( .BOTH. , #452 ) ;
#5749=DIRECTION ( 'NONE',  ( 0.000000000000000000, 0.000000000000000000, -1.000000000000000000 ) ) ;
#5774=DIRECTION ( 'NONE',  ( 0.000000000000000000, 1.000000000000000000, 0.000000000000000000 ) ) ;
#5801=VECTOR ( 'NONE', #16860, 1000.000000000000000 ) ;
#5806=FACE_OUTER_BOUND ( 'NONE', #11322, .T. ) ;
#5833=ORIENTED_EDGE ( 'NONE', *, *, #6366, .F. ) ;
#5882=ORIENTED_EDGE ( 'NONE', *, *, #8451, .F. ) ;
#5891=DIRECTION ( 'NONE',  ( 1.000000000000000000, 0.000000000000000000, -0.000000000000000000 ) ) ;
#5896=AXIS2_PLACEMENT_3D ( 'NONE', #20590, #23802, #5576 ) ;
#5909=CIRCLE ( 'NONE', #5390, 5.200000000000009948 ) ;
#5952=DIRECTION ( 'NONE',  ( -1.000000000000000000, -0.000000000000000000, -0.000000000000000000 ) ) ;
#6046=ORIENTED_EDGE ( 'NONE', *, *, #19905, .F. ) ;
#6047=DIRECTION ( 'NONE',  ( -1.000000000000000000, 0.000000000000000000, 0.000000000000000000 ) ) ;
#6086=DIRECTION ( 'NONE',  ( 1.000000000000000000, 0.000000000000000000, 0.000000000000000000 ) ) ;
#6162=AXIS2_PLACEMENT_3D ( 'NONE', #16045, #59, #8063 ) ;
#6190=AXIS2_PLACEMENT_3D ( 'NONE', #15158, #19761, #14650 ) ;
#6192=CYLINDRICAL_SURFACE ( 'NONE', #12172, 2.500000000000000000 ) ;
#6207=VERTEX_POINT ( 'NONE', #14522 ) ;
#6220=DIRECTION ( 'NONE',  ( 0.000000000000000000, 0.000000000000000000, -1.000000000000000000 ) ) ;
#6279=CARTESIAN_POINT ( 'NONE',  ( -64.50000000000000000, -2.605762844159085212, 20.00000000000000000 ) ) ;
#6320=AXIS2_PLACEMENT_3D ( 'NONE', #4506, #33300, #30411 ) ;
#6336=CARTESIAN_POINT ( 'NONE',  ( -68.50000000000000000, 215.0000000000000000, 2.500000000000000000 ) ) ;
#6366=EDGE_CURVE ( 'NONE', #22231, #23387, #20610, .T. ) ;
#6368=B_SPLINE_CURVE_WITH_KNOTS ( 'NONE', 3,
 ( #33060, #12116, #1894, #7008, #17221, #30345, #22164, #17394, #24732, #1386, #19616, #27608, #14668, #1716, #22507, #27780, #4444, #25231, #9729, #14832, #30512, #5125, #23681, #10419, #18409, #15844, #4958, #8024, #20791, #341 ),
 .UNSPECIFIED., .F., .F.,
 ( 4, 2, 2, 2, 2, 2, 2, 2, 2, 2, 2, 2, 2, 2, 4 ),
 ( 0.007818044621537994371, 0.008306560441632113850, 0.008795076261726231595, 0.009772107901914449737, 0.01026062372200855187, 0.01074913954210265227, 0.01123765536219675440, 0.01172617118229085653, 0.01221468700238495693, 0.01270320282247905906, 0.01319171864257315946, 0.01368023446266726159, 0.01416875028276136372, 0.01465726610285546412, 0.01563429774304366665 ),
 .UNSPECIFIED. ) ;
#6390=EDGE_CURVE ( 'NONE', #9889, #6511, #33667, .T. ) ;
#6391=CARTESIAN_POINT ( 'NONE',  ( -65.20000000000000284, -7.347880794884118356E-15, -19.30000000000003979 ) ) ;
#6407=AXIS2_PLACEMENT_3D ( 'NONE', #12795, #15683, #18246 ) ;
#6421=PRODUCT_DEFINITION_SHAPE ( 'NONE', 'NONE',  #29780 ) ;
#6433=AXIS2_PLACEMENT_3D ( 'NONE', #6627, #17012, #14792 ) ;
#6464=PLANE ( 'NONE',  #6433 ) ;
#6480=ORIENTED_EDGE ( 'NONE', *, *, #6366, .T. ) ;
#6511=VERTEX_POINT ( 'NONE', #21743 ) ;
#6536=CARTESIAN_POINT ( 'NONE',  ( -52.50000000000002132, 155.0000000000000000, 6.938893903907228378E-15 ) ) ;
#6542=DIRECTION ( 'NONE',  ( -0.000000000000000000, -0.000000000000000000, -1.000000000000000000 ) ) ;
#6627=CARTESIAN_POINT ( 'NONE',  ( -68.50000000000000000, 215.0000000000000000, 0.000000000000000000 ) ) ;
#6647=FACE_OUTER_BOUND ( 'NONE', #9460, .T. ) ;
#6648=ORIENTED_EDGE ( 'NONE', *, *, #4323, .F. ) ;
#6701=DIRECTION ( 'NONE',  ( 0.000000000000000000, 0.000000000000000000, 1.000000000000000000 ) ) ;
#6710=DIRECTION ( 'NONE',  ( 0.000000000000000000, 1.000000000000000000, 0.000000000000000000 ) ) ;
#6756=LINE ( 'NONE', #6923, #33653 ) ;
#6806=EDGE_CURVE ( 'NONE', #1695, #22398, #11697, .T. ) ;
#6826=CARTESIAN_POINT ( 'NONE',  ( 60.63708498984762940, 155.0000000000000000, 40.00000000000001421 ) ) ;
#6923=CARTESIAN_POINT ( 'NONE',  ( -64.50000000000000000, 0.000000000000000000, 20.00000000000000000 ) ) ;
#6974=CARTESIAN_POINT ( 'NONE',  ( -64.50000000000000000, 155.0000000000000000, 6.938893903907228378E-15 ) ) ;
#7008=CARTESIAN_POINT ( 'NONE',  ( -57.85233474027615586, 194.9267265987278961, -2.420233332361308332 ) ) ;
#7035=EDGE_CURVE ( 'NONE', #18384, #27919, #31830, .T. ) ;
#7054=CARTESIAN_POINT ( 'NONE',  ( -62.70000000000000284, -88.00000000000000000, -20.00000000000000000 ) ) ;
#7078=ORIENTED_EDGE ( 'NONE', *, *, #25296, .F. ) ;
#7103=CARTESIAN_POINT ( 'NONE',  ( -62.70000000000000284, -88.00000000000000000, -20.00000000000000000 ) ) ;
#7125=FACE_OUTER_BOUND ( 'NONE', #19043, .T. ) ;
#7157=ORIENTED_EDGE ( 'NONE', *, *, #9924, .F. ) ;
#7184=CYLINDRICAL_SURFACE ( 'NONE', #19016, 17.00000000000000355 ) ;
#7246=APPLICATION_CONTEXT ( 'automotive_design' ) ;
#7337=DIRECTION ( 'NONE',  ( -0.000000000000000000, -0.000000000000000000, -1.000000000000000000 ) ) ;
#7346=CARTESIAN_POINT ( 'NONE',  ( -63.49999999999884892, 215.0000000000000000, 2.500000000000000000 ) ) ;
#7380=ORIENTED_EDGE ( 'NONE', *, *, #29747, .T. ) ;
#7415=ORIENTED_EDGE ( 'NONE', *, *, #29527, .T. ) ;
#7454=EDGE_CURVE ( 'NONE', #12774, #19514, #19661, .T. ) ;
#7461=FACE_OUTER_BOUND ( 'NONE', #25505, .T. ) ;
#7496=CARTESIAN_POINT ( 'NONE',  ( -52.50000000000002132, 0.000000000000000000, 270.4495957273638282 ) ) ;
#7551=ORIENTED_EDGE ( 'NONE', *, *, #22218, .F. ) ;
#7562=CARTESIAN_POINT ( 'NONE',  ( -52.50000000000002132, 0.000000000000000000, 20.00000000000001776 ) ) ;
#7576=CARTESIAN_POINT ( 'NONE',  ( -60.91993774119386984, 194.9950632347986641, -0.6485596632537811157 ) ) ;
#7591=ORIENTED_EDGE ( 'NONE', *, *, #13098, .F. ) ;
#7593=ORIENTED_EDGE ( 'NONE', *, *, #17095, .T. ) ;
#7623=EDGE_CURVE ( 'NONE', #610, #23163, #18711, .T. ) ;
#7630=EDGE_LOOP ( 'NONE', ( #17846, #14093, #16426, #11938, #7709, #13815 ) ) ;
#7649=CARTESIAN_POINT ( 'NONE',  ( -65.20000000000000284, -7.347880794884118356E-15, 19.29999999999998295 ) ) ;
#7679=PRESENTATION_STYLE_ASSIGNMENT (( #9893 ) ) ;
#7709=ORIENTED_EDGE ( 'NONE', *, *, #24398, .T. ) ;
#7724=CARTESIAN_POINT ( 'NONE',  ( -67.50001199999999812, 138.8682562219734109, 5.477666192157156999 ) ) ;
#7726=CYLINDRICAL_SURFACE ( 'NONE', #6162, 4.199999999999988631 ) ;
#7734=EDGE_CURVE ( 'NONE', #1695, #25076, #24402, .T. ) ;
#7765=CIRCLE ( 'NONE', #26783, 17.00000000000000355 ) ;
#7804=CARTESIAN_POINT ( 'NONE',  ( -60.00000000000000000, -7.347880794884118356E-15, -20.00000000000001776 ) ) ;
#7833=STYLED_ITEM ( 'NONE', ( #7679 ), #1094 ) ;
#7837=DIRECTION ( 'NONE',  ( 1.000000000000000000, 0.000000000000000000, 0.000000000000000000 ) ) ;
#7848=( NAMED_UNIT ( * ) SI_UNIT ( $, .STERADIAN. ) SOLID_ANGLE_UNIT ( ) );
#7882=CARTESIAN_POINT ( 'NONE',  ( -64.50000000000000000, -95.00000000000000000, 20.00000000000001776 ) ) ;
#7906=ORIENTED_EDGE ( 'NONE', *, *, #32091, .T. ) ;
#7907=CARTESIAN_POINT ( 'NONE',  ( -60.48684543773389066, 194.9711049089068808, 1.526260319620769579 ) ) ;
#7952=CARTESIAN_POINT ( 'NONE',  ( -67.50001199999999812, 172.0000000000000000, 1.112647398146393130 ) ) ;
#7956=ORIENTED_EDGE ( 'NONE', *, *, #26662, .T. ) ;
#7975=DIRECTION ( 'NONE',  ( -1.000000000000000000, 0.000000000000000000, 0.000000000000000000 ) ) ;
#8002=ORIENTED_EDGE ( 'NONE', *, *, #25487, .T. ) ;
#8008=CARTESIAN_POINT ( 'NONE',  ( -58.50000000000002132, 194.9217985566782829, 2.500000000000000000 ) ) ;
#8024=CARTESIAN_POINT ( 'NONE',  ( -57.84141927132884575, 194.9260988872778171, 2.433575273292319707 ) ) ;
#8063=DIRECTION ( 'NONE',  ( -1.000000000000000000, 0.000000000000000000, 0.000000000000000000 ) ) ;
#8086=VERTEX_POINT ( 'NONE', #4451 ) ;
#8139=EDGE_CURVE ( 'NONE', #9805, #18384, #28167, .T. ) ;
#8293=AXIS2_PLACEMENT_3D ( 'NONE', #31550, #11109, #32207 ) ;
#8321=ADVANCED_FACE ( 'NONE', ( #18250 ), #7184, .F. ) ;
#8331=CIRCLE ( 'NONE', #27356, 40.00000000000000711 ) ;
#8343=AXIS2_PLACEMENT_3D ( 'NONE', #737, #897, #14012 ) ;
#8359=FACE_OUTER_BOUND ( 'NONE', #12850, .T. ) ;
#8384=CARTESIAN_POINT ( 'NONE',  ( -52.50000000000002132, 155.0000000000000000, 6.938893903907228378E-15 ) ) ;
#8441=CARTESIAN_POINT ( 'NONE',  ( -67.50001199999998391, 163.5195614605670187, -14.75313718340010460 ) ) ;
#8444=EDGE_LOOP ( 'NONE', ( #25598, #29017 ) ) ;
#8447=CARTESIAN_POINT ( 'NONE',  ( -54.79999999999999716, -6.711064459327494323E-15, 20.00000000000001776 ) ) ;
#8451=EDGE_CURVE ( 'NONE', #28157, #33083, #29357, .T. ) ;
#8555=ADVANCED_FACE ( 'NONE', ( #8359 ), #14660, .T. ) ;
#8617=VECTOR ( 'NONE', #17652, 1000.000000000000114 ) ;
#8739=ADVANCED_FACE ( 'NONE', ( #16512 ), #19244, .T. ) ;
#8872=CARTESIAN_POINT ( 'NONE',  ( 0.000000000000000000, 0.000000000000000000, 0.000000000000000000 ) ) ;
#8895=CIRCLE ( 'NONE', #17612, 37.00000000000000711 ) ;
#8909=EDGE_CURVE ( 'NONE', #8086, #3377, #25032, .T. ) ;
#8963=EDGE_CURVE ( 'NONE', #610, #9889, #22635, .T. ) ;
#9026=LINE ( 'NONE', #19415, #5801 ) ;
#9095=ORIENTED_EDGE ( 'NONE', *, *, #157, .F. ) ;
#9101=CARTESIAN_POINT ( 'NONE',  ( 60.63708498984762940, 155.0000000000000000, 6.938893903907228378E-15 ) ) ;
#9164=ADVANCED_FACE ( 'NONE', ( #18822 ), #11498, .F. ) ;
#9206=AXIS2_PLACEMENT_3D ( 'NONE', #6536, #17428, #3809 ) ;
#9229=LINE ( 'NONE', #22510, #28184 ) ;
#9236=ORIENTED_EDGE ( 'NONE', *, *, #4558, .T. ) ;
#9246=ORIENTED_EDGE ( 'NONE', *, *, #8909, .F. ) ;
#9313=ADVANCED_FACE ( 'NONE', ( #22051 ), #32434, .T. ) ;
#9349=DIRECTION ( 'NONE',  ( 0.000000000000000000, 0.000000000000000000, 1.000000000000000000 ) ) ;
#9390=DIRECTION ( 'NONE',  ( -0.000000000000000000, -0.000000000000000000, -1.000000000000000000 ) ) ;
#9456=FACE_OUTER_BOUND ( 'NONE', #17082, .T. ) ;
#9460=EDGE_LOOP ( 'NONE', ( #25847, #10234, #32942, #19813 ) ) ;
#9521=DIRECTION ( 'NONE',  ( -1.000000000000000000, 0.000000000000000000, 0.000000000000000000 ) ) ;
#9616=CONICAL_SURFACE ( 'NONE', #30286, 37.00000000000000711, 0.7853981633974482790 ) ;
#9631=VECTOR ( 'NONE', #16358, 1000.000000000000000 ) ;
#9655=STYLED_ITEM ( 'NONE', ( #26499 ), #23982 ) ;
#9662=ORIENTED_EDGE ( 'NONE', *, *, #14952, .F. ) ;
#9710=CYLINDRICAL_SURFACE ( 'NONE', #6190, 40.00000000000000711 ) ;
#9729=CARTESIAN_POINT ( 'NONE',  ( -56.12712552280034117, 194.9922069576863066, 0.8039670099889266730 ) ) ;
#9755=DIRECTION ( 'NONE',  ( 0.000000000000000000, -1.000000000000000000, 0.000000000000000000 ) ) ;
#9805=VERTEX_POINT ( 'NONE', #25219 ) ;
#9806=CARTESIAN_POINT ( 'NONE',  ( -67.50000000000000000, 155.0000000000000000, 6.938893903907228378E-15 ) ) ;
#9817=CARTESIAN_POINT ( 'NONE',  ( -63.50000000000001421, 210.0000000000000000, -3.061616997868383141E-16 ) ) ;
#9823=DIRECTION ( 'NONE',  ( 0.000000000000000000, 0.000000000000000000, -1.000000000000000000 ) ) ;
#9832=CARTESIAN_POINT ( 'NONE',  ( -64.50000000000000000, 155.0000000000000000, 6.938893903907228378E-15 ) ) ;
#9889=VERTEX_POINT ( 'NONE', #2564 ) ;
#9893=SURFACE_STYLE_USAGE ( .BOTH. , #12 ) ;
#9922=ORIENTED_EDGE ( 'NONE', *, *, #23228, .F. ) ;
#9924=EDGE_CURVE ( 'NONE', #25076, #9805, #15331, .T. ) ;
#9945=CARTESIAN_POINT ( 'NONE',  ( -58.50000000000002132, 185.0000000000000000, -2.500000000000000000 ) ) ;
#9997=DIRECTION ( 'NONE',  ( 1.000000000000000000, 0.000000000000000000, 0.000000000000000000 ) ) ;
#10005=CONICAL_SURFACE ( 'NONE', #29034, 37.00000000000000711, 0.7853981633974482790 ) ;
#10013=ORIENTED_EDGE ( 'NONE', *, *, #28764, .F. ) ;
#10037=CARTESIAN_POINT ( 'NONE',  ( -52.50000000000002132, -95.00000000000000000, -20.00000000000000000 ) ) ;
#10043=CARTESIAN_POINT ( 'NONE',  ( -64.50000000000000000, -2.605762844159085212, 20.00000000000000000 ) ) ;
#10085=CARTESIAN_POINT ( 'NONE',  ( -58.50000000000002132, 185.0000000000000000, 0.000000000000000000 ) ) ;
#10091=CARTESIAN_POINT ( 'NONE',  ( -52.50000000000002132, 155.0000000000000000, 6.938893903907228378E-15 ) ) ;
#10115=CARTESIAN_POINT ( 'NONE',  ( -67.50001199999999812, 138.5437169723398938, -4.407803664655109976 ) ) ;
#10128=CARTESIAN_POINT ( 'NONE',  ( -60.99994150909498103, 194.9999963443187028, 0.1639972282098350886 ) ) ;
#10146=DIRECTION ( 'NONE',  ( -1.000000000000000000, 0.000000000000000000, 0.000000000000000000 ) ) ;
#10173=CARTESIAN_POINT ( 'NONE',  ( -67.50001199999999812, 169.7531371834000993, 8.519561460567040001 ) ) ;
#10206=CARTESIAN_POINT ( 'NONE',  ( -65.20000000000000284, -0.9203920079924774456, 19.30000000000001847 ) ) ;
#10230=ORIENTED_EDGE ( 'NONE', *, *, #14579, .F. ) ;
#10234=ORIENTED_EDGE ( 'NONE', *, *, #28764, .T. ) ;
#10246=( NAMED_UNIT ( * ) PLANE_ANGLE_UNIT ( ) SI_UNIT ( $, .RADIAN. ) );
#10305=ORIENTED_EDGE ( 'NONE', *, *, #13935, .T. ) ;
#10349=CARTESIAN_POINT ( 'NONE',  ( -67.50001199999998391, 168.5168296348864203, -10.36982646209943759 ) ) ;
#10396=VERTEX_POINT ( 'NONE', #16995 ) ;
#10399=DIRECTION ( 'NONE',  ( 1.000000000000000000, 0.000000000000000000, 0.000000000000000000 ) ) ;
#10419=CARTESIAN_POINT ( 'NONE',  ( -56.84624105109630676, 194.9558714263463912, 1.881936590917415941 ) ) ;
#10442=AXIS2_PLACEMENT_3D ( 'NONE', #21324, #18780, #718 ) ;
#10453=CARTESIAN_POINT ( 'NONE',  ( -67.50001199999998391, 149.5223338078428412, -16.13174377802661752 ) ) ;
#10475=CIRCLE ( 'NONE', #651, 2.500000000000000000 ) ;
#10514=CARTESIAN_POINT ( 'NONE',  ( -67.50001199999999812, 170.2801603273571516, 7.533570508255919229 ) ) ;
#10620=CARTESIAN_POINT ( 'NONE',  ( -67.50001199999998391, 143.7659452401275644, -12.80757580047017896 ) ) ;
#10632=CARTESIAN_POINT ( 'NONE',  ( -59.14727863148851839, 194.9267258542059835, 2.420242894197758510 ) ) ;
#10674=CARTESIAN_POINT ( 'NONE',  ( -67.50001199999999812, 169.7531371834000993, -8.519561460567018685 ) ) ;
#10692=CIRCLE ( 'NONE', #6320, 37.00000000000000711 ) ;
#10723=CARTESIAN_POINT ( 'NONE',  ( -60.00000000000000000, -7.347880794884118356E-15, 20.00000000000001776 ) ) ;
#10738=AXIS2_PLACEMENT_3D ( 'NONE', #12932, #2380, #22645 ) ;
#10765=COLOUR_RGB ( '', 0.40784314, 0.44705882, 0.49803922) ;
#10775=ORIENTED_EDGE ( 'NONE', *, *, #23292, .F. ) ;
#10800=AXIS2_PLACEMENT_3D ( 'NONE', #12371, #13050, #9823 ) ;
#10849=ORIENTED_EDGE ( 'NONE', *, *, #213, .T. ) ;
#10852=FILL_AREA_STYLE_COLOUR ( '', #10765 ) ;
#10886=DIRECTION ( 'NONE',  ( 0.000000000000000000, 0.000000000000000000, -1.000000000000000000 ) ) ;
#10920=VECTOR ( 'NONE', #27059, 1000.000000000000000 ) ;
#10980=CIRCLE ( 'NONE', #30023, 2.500000000000000000 ) ;
#10997=ORIENTED_EDGE ( 'NONE', *, *, #19350, .F. ) ;
#11008=VERTEX_POINT ( 'NONE', #25607 ) ;
#11009=FILL_AREA_STYLE ('',( #10852 ) ) ;
#11029=CARTESIAN_POINT ( 'NONE',  ( -66.50402289005056389, 121.5305141831588003, -17.99597710994943967 ) ) ;
#11096=CIRCLE ( 'NONE', #1313, 5.200000000000002842 ) ;
#11109=DIRECTION ( 'NONE',  ( 0.7071067811865454633, -0.000000000000000000, -0.7071067811865495711 ) ) ;
#11165=ORIENTED_EDGE ( 'NONE', *, *, #23292, .T. ) ;
#11190=CARTESIAN_POINT ( 'NONE',  ( -65.50384660342780307, 120.9385549553365848, -18.99615339657220758 ) ) ;
#11302=AXIS2_PLACEMENT_3D ( 'NONE', #5695, #13533, #15427 ) ;
#11322=EDGE_LOOP ( 'NONE', ( #21305, #24208, #33306, #17801, #1035, #7591, #22602 ) ) ;
#11338=ADVANCED_FACE ( 'NONE', ( #2448 ), #7726, .F. ) ;
#11397=DIRECTION ( 'NONE',  ( 1.000000000000000000, 0.000000000000000000, 0.000000000000000000 ) ) ;
#11398=LINE ( 'NONE', #14277, #10920 ) ;
#11471=ORIENTED_EDGE ( 'NONE', *, *, #12526, .F. ) ;
#11498=PLANE ( 'NONE',  #18345 ) ;
#11564=CARTESIAN_POINT ( 'NONE',  ( -98.16666666666678509, -61.33333333333321491, -13.66666666666659502 ) ) ;
#11588=ORIENTED_EDGE ( 'NONE', *, *, #28872, .F. ) ;
#11631=CARTESIAN_POINT ( 'NONE',  ( -66.50402289005056389, 121.5305141831588003, 17.99597710994943967 ) ) ;
#11678=DIRECTION ( 'NONE',  ( -1.000000000000000000, 0.000000000000000000, 0.000000000000000000 ) ) ;
#11697=LINE ( 'NONE', #14922, #32026 ) ;
#11711=ORIENTED_EDGE ( 'NONE', *, *, #2875, .F. ) ;
#11745=ORIENTED_EDGE ( 'NONE', *, *, #16858, .F. ) ;
#11753=ORIENTED_EDGE ( 'NONE', *, *, #22218, .T. ) ;
#11808=DIRECTION ( 'NONE',  ( 1.000000000000000000, 0.000000000000000000, 0.000000000000000000 ) ) ;
#11809=ADVANCED_FACE ( 'NONE', ( #25565 ), #10005, .T. ) ;
#11856=EDGE_CURVE ( 'NONE', #982, #27043, #21944, .T. ) ;
#11938=ORIENTED_EDGE ( 'NONE', *, *, #14952, .T. ) ;
#11941=DIRECTION ( 'NONE',  ( 0.000000000000000000, 0.000000000000000000, 1.000000000000000000 ) ) ;
#11942=LINE ( 'NONE', #6826, #17919 ) ;
#11971=FACE_OUTER_BOUND ( 'NONE', #199, .T. ) ;
#12030=DIRECTION ( 'NONE',  ( 0.000000000000000000, -1.000000000000000000, 0.000000000000000000 ) ) ;
#12077=DIRECTION ( 'NONE',  ( 0.000000000000000000, -1.000000000000000000, 0.000000000000000000 ) ) ;
#12081=AXIS2_PLACEMENT_3D ( 'NONE', #12145, #11808, #6701 ) ;
#12108=AXIS2_PLACEMENT_3D ( 'NONE', #24106, #23943, #16774 ) ;
#12116=CARTESIAN_POINT ( 'NONE',  ( -58.33685448808505214, 194.9217985566783113, -2.500000000000000444 ) ) ;
#12128=DIRECTION ( 'NONE',  ( -1.000000000000000000, 0.000000000000000000, 0.000000000000000000 ) ) ;
#12145=CARTESIAN_POINT ( 'NONE',  ( -64.50000000000000000, 155.0000000000000000, 6.938893903907228378E-15 ) ) ;
#12166=DIRECTION ( 'NONE',  ( 0.000000000000000000, -1.000000000000000000, 0.000000000000000000 ) ) ;
#12172=AXIS2_PLACEMENT_3D ( 'NONE', #26311, #24247, #5690 ) ;
#12182=FACE_BOUND ( 'NONE', #8444, .T. ) ;
#12197=DIRECTION ( 'NONE',  ( 0.000000000000000000, 0.000000000000000000, 1.000000000000000000 ) ) ;
#12349=FACE_OUTER_BOUND ( 'NONE', #16734, .T. ) ;
#12371=CARTESIAN_POINT ( 'NONE',  ( -52.50000000000002132, 155.0000000000000000, 6.938893903907228378E-15 ) ) ;
#12451=DIRECTION ( 'NONE',  ( 0.000000000000000000, 0.000000000000000000, -1.000000000000000000 ) ) ;
#12492=CARTESIAN_POINT ( 'NONE',  ( -67.50001199999998391, 138.1095834939502822, 2.225267283893263226 ) ) ;
#12526=EDGE_CURVE ( 'NONE', #23163, #610, #6368, .T. ) ;
#12619=CYLINDRICAL_SURFACE ( 'NONE', #26677, 2.500000000000000000 ) ;
#12667=CARTESIAN_POINT ( 'NONE',  ( -58.82767890163440683, 194.9228235633793815, 2.483781759962022218 ) ) ;
#12720=CARTESIAN_POINT ( 'NONE',  ( -67.50001199999999812, 162.5335705082559059, 15.28016032735713736 ) ) ;
#12774=VERTEX_POINT ( 'NONE', #6279 ) ;
#12795=CARTESIAN_POINT ( 'NONE',  ( -63.50000000000001421, 210.0000000000000000, 0.000000000000000000 ) ) ;
#12802=ORIENTED_EDGE ( 'NONE', *, *, #11856, .T. ) ;
#12839=CARTESIAN_POINT ( 'NONE',  ( -58.50000000000002132, 194.9217985566782829, -2.500000000000000000 ) ) ;
#12850=EDGE_LOOP ( 'NONE', ( #1601, #17785, #14942, #26634, #9662, #33348 ) ) ;
#12874=CARTESIAN_POINT ( 'NONE',  ( -64.96121601855533356, 1.809269760319424769, -19.53878398144470907 ) ) ;
#12932=CARTESIAN_POINT ( 'NONE',  ( -58.50000000000001421, -88.00000000000000000, -20.00000000000000000 ) ) ;
#12982=VERTEX_POINT ( 'NONE', #19738 ) ;
#12999=LINE ( 'NONE', #7562, #13405 ) ;
#13014=CARTESIAN_POINT ( 'NONE',  ( -60.87189664283175006, 194.9921494935721569, 0.8066102793772919055 ) ) ;
#13018=ORIENTED_EDGE ( 'NONE', *, *, #19905, .T. ) ;
#13046=CARTESIAN_POINT ( 'NONE',  ( -64.50000000000000000, 2.605762844159070557, -20.00000000000000000 ) ) ;
#13050=DIRECTION ( 'NONE',  ( -1.000000000000000000, -0.000000000000000000, 0.000000000000000000 ) ) ;
#13057=CARTESIAN_POINT ( 'NONE',  ( -67.50001199999999812, 166.2340547598724356, 12.80757580047019495 ) ) ;
#13064=( LENGTH_UNIT ( ) NAMED_UNIT ( * ) SI_UNIT ( .MILLI., .METRE. ) );
#13098=EDGE_CURVE ( 'NONE', #23251, #1081, #3035, .T. ) ;
#13105=ADVANCED_FACE ( 'NONE', ( #17862, #2534 ), #20925, .T. ) ;
#13146=EDGE_CURVE ( 'NONE', #1081, #12774, #646, .T. ) ;
#13151=ORIENTED_EDGE ( 'NONE', *, *, #7623, .F. ) ;
#13159=CIRCLE ( 'NONE', #12081, 40.00000000000000711 ) ;
#13203=AXIS2_PLACEMENT_3D ( 'NONE', #9832, #4884, #19872 ) ;
#13266=ORIENTED_EDGE ( 'NONE', *, *, #22463, .F. ) ;
#13321=DIRECTION ( 'NONE',  ( -1.000000000000000000, 0.000000000000000000, 0.000000000000000000 ) ) ;
#13391=UNCERTAINTY_MEASURE_WITH_UNIT (LENGTH_MEASURE( 1.000000000000000082E-05 ), #17898, 'distance_accuracy_value', 'NONE');
#13405=VECTOR ( 'NONE', #57, 1000.000000000000000 ) ;
#13524=DIRECTION ( 'NONE',  ( -1.000000000000000000, -0.000000000000000000, -0.000000000000000000 ) ) ;
#13533=DIRECTION ( 'NONE',  ( 0.000000000000000000, -1.000000000000000000, 0.000000000000000000 ) ) ;
#13556=APPLICATION_CONTEXT ( 'automotive_design' ) ;
#13636=FACE_OUTER_BOUND ( 'NONE', #3333, .T. ) ;
#13721=CIRCLE ( 'NONE', #13203, 40.00000000000000711 ) ;
#13781=AXIS2_PLACEMENT_3D ( 'NONE', #17418, #22535, #30203 ) ;
#13815=ORIENTED_EDGE ( 'NONE', *, *, #4323, .T. ) ;
#13876=DIRECTION ( 'NONE',  ( 0.7071067811865475727, 0.7071067811865475727, 0.000000000000000000 ) ) ;
#13929=EDGE_CURVE ( 'NONE', #18293, #161, #10475, .T. ) ;
#13932=CARTESIAN_POINT ( 'NONE',  ( -58.50000000000001421, -88.00000000000000000, 20.00000000000000000 ) ) ;
#13935=EDGE_CURVE ( 'NONE', #6207, #26026, #13159, .T. ) ;
#13958=CARTESIAN_POINT ( 'NONE',  ( -52.50000000000002132, 155.0000000000000000, 17.00000000000001066 ) ) ;
#13979=AXIS2_PLACEMENT_3D ( 'NONE', #31654, #15653, #5749 ) ;
#13993=AXIS2_PLACEMENT_3D ( 'NONE', #9806, #10146, #22917 ) ;
#14012=DIRECTION ( 'NONE',  ( 0.000000000000000000, 0.000000000000000000, -1.000000000000000000 ) ) ;
#14034=DIRECTION ( 'NONE',  ( -1.000000000000000000, 0.000000000000000000, 0.000000000000000000 ) ) ;
#14093=ORIENTED_EDGE ( 'NONE', *, *, #13929, .F. ) ;
#14133=VERTEX_POINT ( 'NONE', #19978 ) ;
#14139=CARTESIAN_POINT ( 'NONE',  ( -58.50000000000002132, 194.9217985566782829, -2.500000000000000000 ) ) ;
#14220=CARTESIAN_POINT ( 'NONE',  ( -67.50001200000001234, 156.1126473981464642, -16.99999999999999645 ) ) ;
#14277=CARTESIAN_POINT ( 'NONE',  ( -64.50000000000000000, 0.000000000000000000, -20.00000000000000000 ) ) ;
#14344=CARTESIAN_POINT ( 'NONE',  ( -65.20000000000000284, -7.347880794884118356E-15, -19.30000000000003979 ) ) ;
#14352=CARTESIAN_POINT ( 'NONE',  ( -67.50000000000000000, 122.1366465496900275, 17.00000000000001421 ) ) ;
#14353=ORIENTED_EDGE ( 'NONE', *, *, #18063, .T. ) ;
#14381=LINE ( 'NONE', #7054, #26988 ) ;
#14436=ADVANCED_FACE ( 'NONE', ( #5806 ), #26269, .F. ) ;
#14509=ORIENTED_EDGE ( 'NONE', *, *, #21802, .T. ) ;
#14522=CARTESIAN_POINT ( 'NONE',  ( -64.50000000000000000, 155.0000000000000000, 40.00000000000001421 ) ) ;
#14530=FACE_OUTER_BOUND ( 'NONE', #2688, .T. ) ;
#14544=EDGE_LOOP ( 'NONE', ( #6648, #11753, #9236, #16023, #11588 ) ) ;
#14579=EDGE_CURVE ( 'NONE', #10396, #33071, #7765, .T. ) ;
#14650=DIRECTION ( 'NONE',  ( 0.000000000000000000, 0.000000000000000000, 1.000000000000000000 ) ) ;
#14660=TOROIDAL_SURFACE ( 'NONE', #15756, 4.999999999999990230, 2.500000000000000000 ) ;
#14668=CARTESIAN_POINT ( 'NONE',  ( -56.08018104464575515, 194.9950560901275480, -0.6488614982153378952 ) ) ;
#14682=EDGE_CURVE ( 'NONE', #14133, #25683, #22601, .T. ) ;
#14762=VECTOR ( 'NONE', #6710, 1000.000000000000000 ) ;
#14792=DIRECTION ( 'NONE',  ( 0.000000000000000000, 0.000000000000000000, -1.000000000000000000 ) ) ;
#14832=CARTESIAN_POINT ( 'NONE',  ( -56.25248981486732447, 194.9849645003486387, 1.107065583161625621 ) ) ;
#14839=VECTOR ( 'NONE', #5952, 1000.000000000000000 ) ;
#14840=CARTESIAN_POINT ( 'NONE',  ( -65.20000000000000284, -0.9203920079924744480, -19.30000000000004690 ) ) ;
#14922=CARTESIAN_POINT ( 'NONE',  ( -67.50000000000000000, -92.00000000000000000, 270.4495957273638282 ) ) ;
#14942=ORIENTED_EDGE ( 'NONE', *, *, #28872, .T. ) ;
#14949=CARTESIAN_POINT ( 'NONE',  ( -67.50000000000000000, 122.1366465496900275, 17.00000000000001421 ) ) ;
#14951=DIRECTION ( 'NONE',  ( -1.000000000000000000, 0.000000000000000000, 0.000000000000000000 ) ) ;
#14952=EDGE_CURVE ( 'NONE', #6511, #11008, #24607, .T. ) ;
#14956=CARTESIAN_POINT ( 'NONE',  ( -64.50000000000000000, 0.000000000000000000, -20.00000000000000000 ) ) ;
#14987=CARTESIAN_POINT ( 'NONE',  ( -64.50000000000000000, -95.00000000000000000, -20.00000000000000000 ) ) ;
#15042=AXIS2_PLACEMENT_3D ( 'NONE', #7804, #465, #7975 ) ;
#15053=CARTESIAN_POINT ( 'NONE',  ( -58.66318290517560996, 194.9217985566783113, -2.499999999999999556 ) ) ;
#15065=VECTOR ( 'NONE', #3887, 1000.000000000000114 ) ;
#15131=DIRECTION ( 'NONE',  ( 0.000000000000000000, 0.000000000000000000, -1.000000000000000000 ) ) ;
#15156=DIRECTION ( 'NONE',  ( 0.000000000000000000, 0.000000000000000000, -1.000000000000000000 ) ) ;
#15158=CARTESIAN_POINT ( 'NONE',  ( 60.63708498984762940, 155.0000000000000000, 6.938893903907228378E-15 ) ) ;
#15256=CARTESIAN_POINT ( 'NONE',  ( -54.30000000000002558, -88.00000000000000000, 20.00000000000000000 ) ) ;
#15286=CYLINDRICAL_SURFACE ( 'NONE', #24881, 4.199999999999988631 ) ;
#15301=CARTESIAN_POINT ( 'NONE',  ( -64.50000000000000000, 2.605762844159070557, 20.00000000000000000 ) ) ;
#15316=DIRECTION ( 'NONE',  ( 1.000000000000000000, 0.000000000000000000, -0.000000000000000000 ) ) ;
#15331=LINE ( 'NONE', #28622, #33596 ) ;
#15381=CARTESIAN_POINT ( 'NONE',  ( -67.50001199999998391, 152.7747327161067403, 16.89041650604971068 ) ) ;
#15394=CARTESIAN_POINT ( 'NONE',  ( -60.02503143742045921, 194.9506873066471542, -1.987662087495396301 ) ) ;
#15416=ORIENTED_EDGE ( 'NONE', *, *, #4558, .F. ) ;
#15419=VECTOR ( 'NONE', #9755, 1000.000000000000000 ) ;
#15427=DIRECTION ( 'NONE',  ( 0.000000000000000000, -0.000000000000000000, -1.000000000000000000 ) ) ;
#15444=CARTESIAN_POINT ( 'NONE',  ( -67.50001199999999812, 171.8904165060497178, -2.225267283893245907 ) ) ;
#15449=AXIS2_PLACEMENT_3D ( 'NONE', #5635, #26742, #16348 ) ;
#15450=EDGE_LOOP ( 'NONE', ( #16684, #30451, #30377, #1455 ) ) ;
#15492=ORIENTED_EDGE ( 'NONE', *, *, #13098, .T. ) ;
#15497=CARTESIAN_POINT ( 'NONE',  ( -64.50000000000000000, 155.0000000000000000, -40.00000000000000000 ) ) ;
#15521=CARTESIAN_POINT ( 'NONE',  ( -67.50000599999999906, 155.0000000000000000, 17.00000000000001421 ) ) ;
#15534=B_SPLINE_CURVE_WITH_KNOTS ( 'NONE', 3,
 ( #1401, #3792, #11631, #14352 ),
 .UNSPECIFIED., .F., .F.,
 ( 4, 4 ),
 ( 0.000000000000000000, 0.004600009204204579850 ),
 .UNSPECIFIED. ) ;
#15557=CARTESIAN_POINT ( 'NONE',  ( -60.66914996032592455, 194.9805833264304908, -1.253524243223063994 ) ) ;
#15567=EDGE_LOOP ( 'NONE', ( #30562, #10849, #28280, #22698 ) ) ;
#15575=EDGE_LOOP ( 'NONE', ( #7551, #27971, #7078, #27178, #32119 ) ) ;
#15653=DIRECTION ( 'NONE',  ( 1.000000000000000000, 0.000000000000000000, 0.000000000000000000 ) ) ;
#15661=EDGE_LOOP ( 'NONE', ( #24116, #1242 ) ) ;
#15683=DIRECTION ( 'NONE',  ( 0.000000000000000000, 0.000000000000000000, 1.000000000000000000 ) ) ;
#15756=AXIS2_PLACEMENT_3D ( 'NONE', #5629, #3236, #18908 ) ;
#15772=CARTESIAN_POINT ( 'NONE',  ( -67.50001199999999812, 171.8904165060497178, 2.225267283893263226 ) ) ;
#15844=CARTESIAN_POINT ( 'NONE',  ( -57.24471460971760450, 194.9412964752286825, 2.168227419017068502 ) ) ;
#15955=DIRECTION ( 'NONE',  ( 0.000000000000000000, 0.000000000000000000, 1.000000000000000000 ) ) ;
#15968=DIRECTION ( 'NONE',  ( -0.000000000000000000, -0.000000000000000000, -1.000000000000000000 ) ) ;
#16013=DIRECTION ( 'NONE',  ( 0.000000000000000000, 0.000000000000000000, -1.000000000000000000 ) ) ;
#16023=ORIENTED_EDGE ( 'NONE', *, *, #29115, .F. ) ;
#16029=EDGE_LOOP ( 'NONE', ( #5706, #13151, #22359, #30246, #17795 ) ) ;
#16045=CARTESIAN_POINT ( 'NONE',  ( -58.50000000000001421, -88.00000000000000000, -20.00000000000000000 ) ) ;
#16079=FACE_OUTER_BOUND ( 'NONE', #14544, .T. ) ;
#16091=CARTESIAN_POINT ( 'NONE',  ( -65.20000000000000284, -7.347880794884118356E-15, 270.4495957273638282 ) ) ;
#16099=CARTESIAN_POINT ( 'NONE',  ( -67.50001199999999812, 165.3698264620994678, -13.51682963488642919 ) ) ;
#16102=ORIENTED_EDGE ( 'NONE', *, *, #32091, .F. ) ;
#16187=EDGE_CURVE ( 'NONE', #20653, #28109, #8895, .T. ) ;
#16201=ORIENTED_EDGE ( 'NONE', *, *, #1028, .F. ) ;
#16229=ORIENTED_EDGE ( 'NONE', *, *, #19116, .T. ) ;
#16238=DIRECTION ( 'NONE',  ( 0.000000000000000000, 0.000000000000000000, 1.000000000000000000 ) ) ;
#16283=VERTEX_POINT ( 'NONE', #6336 ) ;
#16348=DIRECTION ( 'NONE',  ( 0.000000000000000000, 0.000000000000000000, -1.000000000000000000 ) ) ;
#16354=CARTESIAN_POINT ( 'NONE',  ( -60.00000000000000000, -7.347880794884118356E-15, 270.4495957273638282 ) ) ;
#16356=EDGE_LOOP ( 'NONE', ( #21931, #4638 ) ) ;
#16358=DIRECTION ( 'NONE',  ( 0.000000000000000000, 0.000000000000000000, -1.000000000000000000 ) ) ;
#16426=ORIENTED_EDGE ( 'NONE', *, *, #17276, .F. ) ;
#16439=DIRECTION ( 'NONE',  ( 0.000000000000000000, 0.000000000000000000, 1.000000000000000000 ) ) ;
#16493=CARTESIAN_POINT ( 'NONE',  ( -67.50000000000000000, 155.0000000000000000, 6.938893903907228378E-15 ) ) ;
#16512=FACE_OUTER_BOUND ( 'NONE', #15575, .T. ) ;
#16596=ORIENTED_EDGE ( 'NONE', *, *, #7454, .T. ) ;
#16647=EDGE_CURVE ( 'NONE', #16283, #4641, #5643, .T. ) ;
#16684=ORIENTED_EDGE ( 'NONE', *, *, #26662, .F. ) ;
#16690=VECTOR ( 'NONE', #13524, 1000.000000000000000 ) ;
#16700=CIRCLE ( 'NONE', #10738, 4.199999999999988631 ) ;
#16734=EDGE_LOOP ( 'NONE', ( #5063, #26915, #27584, #3292, #22377, #7956 ) ) ;
#16751=PRODUCT ( 'pad arm right_right', 'pad arm right_right', '', ( #3058 ) ) ;
#16774=DIRECTION ( 'NONE',  ( 0.000000000000000000, 0.000000000000000000, -1.000000000000000000 ) ) ;
#16815=EDGE_LOOP ( 'NONE', ( #4464, #16229 ) ) ;
#16845=VECTOR ( 'NONE', #21213, 1000.000000000000000 ) ;
#16858=EDGE_CURVE ( 'NONE', #20297, #6207, #13721, .T. ) ;
#16860=DIRECTION ( 'NONE',  ( 1.000000000000000000, -0.000000000000000000, -0.000000000000000000 ) ) ;
#16953=CARTESIAN_POINT ( 'NONE',  ( -52.50000000000002132, 155.0000000000000000, 40.00000000000001421 ) ) ;
#16995=CARTESIAN_POINT ( 'NONE',  ( -52.50000000000002132, 155.0000000000000000, 17.00000000000001066 ) ) ;
#17012=DIRECTION ( 'NONE',  ( 1.000000000000000000, 0.000000000000000000, 0.000000000000000000 ) ) ;
#17070=AXIS2_PLACEMENT_3D ( 'NONE', #24754, #26962, #16238 ) ;
#17082=EDGE_LOOP ( 'NONE', ( #10013, #21303, #20095, #23909 ) ) ;
#17095=EDGE_CURVE ( 'NONE', #30404, #18396, #24791, .T. ) ;
#17164=LINE ( 'NONE', #17339, #29236 ) ;
#17187=DIRECTION ( 'NONE',  ( 0.000000000000000000, 0.000000000000000000, 1.000000000000000000 ) ) ;
#17200=VERTEX_POINT ( 'NONE', #21882 ) ;
#17221=CARTESIAN_POINT ( 'NONE',  ( -57.69437687863553776, 194.9296432668266732, -2.372230612754127499 ) ) ;
#17276=EDGE_CURVE ( 'NONE', #6511, #18293, #22984, .T. ) ;
#17305=CIRCLE ( 'NONE', #31440, 2.500000000000000000 ) ;
#17339=CARTESIAN_POINT ( 'NONE',  ( 60.63708498984762940, 120.3589838486224579, -20.00000000000000000 ) ) ;
#17394=CARTESIAN_POINT ( 'NONE',  ( -56.61815514298172758, 194.9659613751070140, -1.653849335561433209 ) ) ;
#17416=ORIENTED_EDGE ( 'NONE', *, *, #13146, .T. ) ;
#17418=CARTESIAN_POINT ( 'NONE',  ( -58.50000000000002132, 185.0000000000000000, 0.000000000000000000 ) ) ;
#17428=DIRECTION ( 'NONE',  ( -1.000000000000000000, -0.000000000000000000, -0.000000000000000000 ) ) ;
#17507=DIRECTION ( 'NONE',  ( 0.000000000000000000, 1.000000000000000000, 0.000000000000000000 ) ) ;
#17540=CARTESIAN_POINT ( 'NONE',  ( -63.49999999999884892, 215.0000000000000000, -2.500000000000000000 ) ) ;
#17588=CYLINDRICAL_SURFACE ( 'NONE', #13781, 2.500000000000000000 ) ;
#17598=CARTESIAN_POINT ( 'NONE',  ( -67.50001199999998391, 138.1095834939503106, -2.225267283893253012 ) ) ;
#17612=AXIS2_PLACEMENT_3D ( 'NONE', #27293, #12128, #25074 ) ;
#17616=CARTESIAN_POINT ( 'NONE',  ( -59.30608239026425821, 194.9296489543815483, 2.372148111071822996 ) ) ;
#17632=VECTOR ( 'NONE', #7337, 1000.000000000000000 ) ;
#17652=DIRECTION ( 'NONE',  ( 0.7071067811865474617, 8.659560562354932858E-17, 0.7071067811865474617 ) ) ;
#17677=CARTESIAN_POINT ( 'NONE',  ( -58.50000000000001421, -88.00000000000000000, -20.00000000000000000 ) ) ;
#17741=CARTESIAN_POINT ( 'NONE',  ( -52.50000000000002132, 155.0000000000000000, 6.938893903907228378E-15 ) ) ;
#17749=ORIENTED_EDGE ( 'NONE', *, *, #16187, .F. ) ;
#17754=CARTESIAN_POINT ( 'NONE',  ( -54.30000000000002558, -88.00000000000000000, -20.00000000000000000 ) ) ;
#17763=CLOSED_SHELL ( 'NONE', ( #8555, #11338, #33480, #21398, #30761, #31230, #11809, #24796, #19938, #9313, #24389, #24485, #27217, #23467, #21442, #13105, #1244, #23566, #14436, #31457, #9164, #8321, #8739, #28651, #5149, #29130, #1055 ) ) ;
#17766=CARTESIAN_POINT ( 'NONE',  ( -67.50001199999998391, 147.4664294917440373, -15.28016032735712848 ) ) ;
#17780=CARTESIAN_POINT ( 'NONE',  ( -60.91988776943159678, 194.9950600780878460, 0.6490123436103525378 ) ) ;
#17785=ORIENTED_EDGE ( 'NONE', *, *, #25206, .T. ) ;
#17795=ORIENTED_EDGE ( 'NONE', *, *, #17276, .T. ) ;
#17801=ORIENTED_EDGE ( 'NONE', *, *, #7454, .F. ) ;
#17846=ORIENTED_EDGE ( 'NONE', *, *, #25206, .F. ) ;
#17862=FACE_BOUND ( 'NONE', #26246, .T. ) ;
#17889=DIRECTION ( 'NONE',  ( -0.000000000000000000, -0.000000000000000000, -1.000000000000000000 ) ) ;
#17898=( LENGTH_UNIT ( ) NAMED_UNIT ( * ) SI_UNIT ( .MILLI., .METRE. ) );
#17919=VECTOR ( 'NONE', #22324, 1000.000000000000000 ) ;
#17939=AXIS2_PLACEMENT_3D ( 'NONE', #10091, #27961, #1903 ) ;
#17948=CARTESIAN_POINT ( 'NONE',  ( -67.50001199999999812, 152.7747327161067403, -16.89041650604970002 ) ) ;
#17962=CARTESIAN_POINT ( 'NONE',  ( -60.74744875717816939, 194.9849611312037041, -1.107162489773501513 ) ) ;
#18063=EDGE_CURVE ( 'NONE', #161, #9889, #29541, .T. ) ;
#18233=SURFACE_STYLE_FILL_AREA ( #31178 ) ;
#18246=DIRECTION ( 'NONE',  ( 1.000000000000000000, 0.000000000000000000, 0.000000000000000000 ) ) ;
#18250=FACE_OUTER_BOUND ( 'NONE', #33047, .T. ) ;
#18293=VERTEX_POINT ( 'NONE', #27627 ) ;
#18345=AXIS2_PLACEMENT_3D ( 'NONE', #24612, #13876, #21876 ) ;
#18354=EDGE_CURVE ( 'NONE', #12982, #19514, #1115, .T. ) ;
#18383=VECTOR ( 'NONE', #14034, 1000.000000000000000 ) ;
#18384=VERTEX_POINT ( 'NONE', #6391 ) ;
#18396=VERTEX_POINT ( 'NONE', #3833 ) ;
#18405=VECTOR ( 'NONE', #24517, 1000.000000000000000 ) ;
#18409=CARTESIAN_POINT ( 'NONE',  ( -56.97195197156149504, 194.9507991595696694, 1.985452284598899553 ) ) ;
#18431=VECTOR ( 'NONE', #22461, 1000.000000000000000 ) ;
#18550=ORIENTED_EDGE ( 'NONE', *, *, #29747, .F. ) ;
#18551=ORIENTED_EDGE ( 'NONE', *, *, #7035, .T. ) ;
#18569=CARTESIAN_POINT ( 'NONE',  ( -58.50000000000001421, -88.00000000000000000, 20.00000000000000000 ) ) ;
#18596=DIRECTION ( 'NONE',  ( -0.000000000000000000, -0.000000000000000000, -1.000000000000000000 ) ) ;
#18711=B_SPLINE_CURVE_WITH_KNOTS ( 'NONE', 3,
 ( #4838, #28352, #12667, #10632, #17616, #28677, #23064, #4669, #33456, #20341, #7907, #30740, #28522, #13014, #17780, #23571, #10128, #20508, #30911, #7576, #2794, #17962, #15557, #23406, #5006, #240, #15394, #2123, #25793, #69, #2458, #30563, #15053, #12839 ),
 .UNSPECIFIED., .F., .F.,
 ( 4, 2, 2, 2, 2, 2, 2, 2, 2, 2, 2, 2, 2, 2, 2, 2, 4 ),
 ( 0.000000000000000000, 0.0004886277888461246482, 0.0009772555776922492964, 0.001465883366538373945, 0.001954511155384498593, 0.002443138944230623458, 0.002931766733076747889, 0.003420394521922872320, 0.003909022310768997185, 0.004397650099615122050, 0.004886277888461246915, 0.005374905677307370913, 0.005863533466153495778, 0.006352161254999620643, 0.006840789043845744641, 0.007329416832691869506, 0.007818044621537994371 ),
 .UNSPECIFIED. ) ;
#18780=DIRECTION ( 'NONE',  ( 1.000000000000000000, 0.000000000000000000, 0.000000000000000000 ) ) ;
#18792=ORIENTED_EDGE ( 'NONE', *, *, #27006, .T. ) ;
#18815=ORIENTED_EDGE ( 'NONE', *, *, #14682, .T. ) ;
#18822=FACE_OUTER_BOUND ( 'NONE', #20107, .T. ) ;
#18908=DIRECTION ( 'NONE',  ( 1.000000000000000000, 0.000000000000000000, 0.000000000000000000 ) ) ;
#18951=CIRCLE ( 'NONE', #3716, 7.499999999999992895 ) ;
#19009=( NAMED_UNIT ( * ) SI_UNIT ( $, .STERADIAN. ) SOLID_ANGLE_UNIT ( ) );
#19016=AXIS2_PLACEMENT_3D ( 'NONE', #17741, #25912, #20294 ) ;
#19043=EDGE_LOOP ( 'NONE', ( #27475, #7157, #23194, #26923, #18815, #11711, #33385 ) ) ;
#19048=DIRECTION ( 'NONE',  ( 0.000000000000000000, 0.000000000000000000, 1.000000000000000000 ) ) ;
#19100=DIRECTION ( 'NONE',  ( 0.000000000000000000, 0.000000000000000000, 1.000000000000000000 ) ) ;
#19116=EDGE_CURVE ( 'NONE', #33071, #10396, #20869, .T. ) ;
#19171=CYLINDRICAL_SURFACE ( 'NONE', #28175, 40.00000000000000711 ) ;
#19244=CYLINDRICAL_SURFACE ( 'NONE', #29915, 2.500000000000000000 ) ;
#19325=EDGE_CURVE ( 'NONE', #14133, #1695, #2257, .T. ) ;
#19350=EDGE_CURVE ( 'NONE', #27043, #23387, #27468, .T. ) ;
#19388=AXIS2_PLACEMENT_3D ( 'NONE', #14956, #27555, #17507 ) ;
#19415=CARTESIAN_POINT ( 'NONE',  ( 60.63708498984762940, 120.3589838486224437, 20.00000000000000000 ) ) ;
#19514=VERTEX_POINT ( 'NONE', #7882 ) ;
#19616=CARTESIAN_POINT ( 'NONE',  ( -56.25402757683428234, 194.9848779240976171, -1.110136720165091129 ) ) ;
#19661=LINE ( 'NONE', #30051, #26595 ) ;
#19672=CARTESIAN_POINT ( 'NONE',  ( -56.00000000000002132, 209.9999999999999716, 0.000000000000000000 ) ) ;
#19738=CARTESIAN_POINT ( 'NONE',  ( -52.50000000000002132, -95.00000000000000000, 20.00000000000001776 ) ) ;
#19761=DIRECTION ( 'NONE',  ( -1.000000000000000000, 0.000000000000000000, 0.000000000000000000 ) ) ;
#19784=CARTESIAN_POINT ( 'NONE',  ( -68.50000000000000000, 215.0000000000000000, -2.500000000000000000 ) ) ;
#19813=ORIENTED_EDGE ( 'NONE', *, *, #2461, .F. ) ;
#19847=ORIENTED_EDGE ( 'NONE', *, *, #29742, .F. ) ;
#19872=DIRECTION ( 'NONE',  ( 0.000000000000000000, 0.000000000000000000, 1.000000000000000000 ) ) ;
#19905=EDGE_CURVE ( 'NONE', #23990, #22576, #32532, .T. ) ;
#19938=ADVANCED_FACE ( 'NONE', ( #1699, #6647 ), #9710, .T. ) ;
#19978=CARTESIAN_POINT ( 'NONE',  ( -67.50000000000000000, 122.1366465496900418, -17.00000000000001421 ) ) ;
#20095=ORIENTED_EDGE ( 'NONE', *, *, #1028, .T. ) ;
#20107=EDGE_LOOP ( 'NONE', ( #18792, #2337, #5060, #1697 ) ) ;
#20181=ORIENTED_EDGE ( 'NONE', *, *, #18354, .F. ) ;
#20198=DIRECTION ( 'NONE',  ( 1.000000000000000000, 0.000000000000000000, 0.000000000000000000 ) ) ;
#20206=EDGE_CURVE ( 'NONE', #23990, #12774, #11096, .T. ) ;
#20294=DIRECTION ( 'NONE',  ( 0.000000000000000000, 0.000000000000000000, 1.000000000000000000 ) ) ;
#20297=VERTEX_POINT ( 'NONE', #15497 ) ;
#20333=CARTESIAN_POINT ( 'NONE',  ( -67.50000000000000000, 0.000000000000000000, 17.00000000000001421 ) ) ;
#20341=CARTESIAN_POINT ( 'NONE',  ( -60.38337337305365793, 194.9660334721754111, 1.652118058477962004 ) ) ;
#20435=FACE_OUTER_BOUND ( 'NONE', #23036, .T. ) ;
#20451=SHAPE_REPRESENTATION_RELATIONSHIP ( 'NONE' , 'NONE' ,  #30038, #1094 ) ;
#20494=CARTESIAN_POINT ( 'NONE',  ( -67.50001199999998391, 144.6301735379005038, 13.51682963488643807 ) ) ;
#20508=CARTESIAN_POINT ( 'NONE',  ( -61.00005817115211926, 195.0000036356967712, -0.1622090645192997005 ) ) ;
#20551=CARTESIAN_POINT ( 'NONE',  ( -63.50000000000004263, 215.0000000000000000, -2.500000000000000000 ) ) ;
#20590=CARTESIAN_POINT ( 'NONE',  ( -58.50000000000002132, 209.9999999999999716, 0.000000000000000000 ) ) ;
#20610=CIRCLE ( 'NONE', #22224, 4.199999999999988631 ) ;
#20653=VERTEX_POINT ( 'NONE', #14949 ) ;
#20750=CARTESIAN_POINT ( 'NONE',  ( -64.96121601855533356, -1.809269760319447418, 19.53878398144468775 ) ) ;
#20791=CARTESIAN_POINT ( 'NONE',  ( -58.16962743627800592, 194.9217985566782829, 2.500000000000000000 ) ) ;
#20827=CARTESIAN_POINT ( 'NONE',  ( -67.50001199999998391, 146.4804385394329529, -14.75313718340010460 ) ) ;
#20869=CIRCLE ( 'NONE', #17070, 17.00000000000000355 ) ;
#20880=MECHANICAL_DESIGN_GEOMETRIC_PRESENTATION_REPRESENTATION('',(#7833),#32298);
#20894=CARTESIAN_POINT ( 'NONE',  ( -67.50001199999998391, 171.4562830276601346, -4.407803664655100206 ) ) ;
#20925=PLANE ( 'NONE',  #32305 ) ;
#21053=CARTESIAN_POINT ( 'NONE',  ( -67.50001199999999812, 167.8075758004701754, -11.23405475987242497 ) ) ;
#21200=VECTOR ( 'NONE', #12077, 1000.000000000000000 ) ;
#21213=DIRECTION ( 'NONE',  ( 0.000000000000000000, 1.000000000000000000, 0.000000000000000000 ) ) ;
#21303=ORIENTED_EDGE ( 'NONE', *, *, #23557, .T. ) ;
#21305=ORIENTED_EDGE ( 'NONE', *, *, #22463, .T. ) ;
#21324=CARTESIAN_POINT ( 'NONE',  ( -63.49999999999884892, 215.0000000000003979, 0.000000000000000000 ) ) ;
#21391=VECTOR ( 'NONE', #1737, 1000.000000000000000 ) ;
#21398=ADVANCED_FACE ( 'NONE', ( #1741 ), #17588, .T. ) ;
#21442=ADVANCED_FACE ( 'NONE', ( #11971 ), #32745, .F. ) ;
#21550=CARTESIAN_POINT ( 'NONE',  ( -125.0000000000000000, -95.00000000000000000, 20.00000000000001776 ) ) ;
#21671=AXIS2_PLACEMENT_3D ( 'NONE', #13932, #19048, #6086 ) ;
#21687=PRODUCT_DEFINITION_CONTEXT ( 'detailed design', #13556, 'design' ) ;
#21743=CARTESIAN_POINT ( 'NONE',  ( -61.00000000000002842, 209.9999999999999716, -3.061616997868380183E-16 ) ) ;
#21802=EDGE_CURVE ( 'NONE', #982, #22231, #14381, .T. ) ;
#21840=CIRCLE ( 'NONE', #10442, 2.500000000000000000 ) ;
#21860=CARTESIAN_POINT ( 'NONE',  ( -67.50000000000000000, 155.0000000000000000, -37.00000000000000000 ) ) ;
#21866=DIRECTION ( 'NONE',  ( -0.000000000000000000, -0.000000000000000000, -1.000000000000000000 ) ) ;
#21876=DIRECTION ( 'NONE',  ( 0.000000000000000000, 0.000000000000000000, -1.000000000000000000 ) ) ;
#21882=CARTESIAN_POINT ( 'NONE',  ( -52.50000000000002132, 155.0000000000000000, -40.00000000000000000 ) ) ;
#21931=ORIENTED_EDGE ( 'NONE', *, *, #11856, .F. ) ;
#21944=CIRCLE ( 'NONE', #5107, 4.199999999999988631 ) ;
#22051=FACE_OUTER_BOUND ( 'NONE', #25713, .T. ) ;
#22128=CARTESIAN_POINT ( 'NONE',  ( -63.50000000000004263, 215.0000000000000000, 0.000000000000000000 ) ) ;
#22164=CARTESIAN_POINT ( 'NONE',  ( -56.96409840163092753, 194.9506684299840913, -1.999309141333601492 ) ) ;
#22172=DIRECTION ( 'NONE',  ( -0.000000000000000000, -0.000000000000000000, -1.000000000000000000 ) ) ;
#22218=EDGE_CURVE ( 'NONE', #24997, #4641, #2330, .T. ) ;
#22224=AXIS2_PLACEMENT_3D ( 'NONE', #142, #15968, #25867 ) ;
#22231=VERTEX_POINT ( 'NONE', #7103 ) ;
#22324=DIRECTION ( 'NONE',  ( -1.000000000000000000, 0.000000000000000000, 0.000000000000000000 ) ) ;
#22354=ORIENTED_EDGE ( 'NONE', *, *, #8139, .T. ) ;
#22359=ORIENTED_EDGE ( 'NONE', *, *, #8963, .T. ) ;
#22377=ORIENTED_EDGE ( 'NONE', *, *, #157, .T. ) ;
#22398=VERTEX_POINT ( 'NONE', #894 ) ;
#22461=DIRECTION ( 'NONE',  ( -1.000000000000000000, 0.000000000000000000, 0.000000000000000000 ) ) ;
#22463=EDGE_CURVE ( 'NONE', #26026, #20653, #15534, .T. ) ;
#22505=COLOUR_RGB ( '', 0.40784314, 0.44705882, 0.49803922) ;
#22507=CARTESIAN_POINT ( 'NONE',  ( -56.00013514549282689, 194.9999915534094725, -0.1669880218061202404 ) ) ;
#22510=CARTESIAN_POINT ( 'NONE',  ( -52.50000000000002132, -95.00000000000000000, 270.4495957273638282 ) ) ;
#22535=DIRECTION ( 'NONE',  ( 0.000000000000000000, 1.000000000000000000, 0.000000000000000000 ) ) ;
#22550=LINE ( 'NONE', #9945, #14762 ) ;
#22576=VERTEX_POINT ( 'NONE', #24908 ) ;
#22601=B_SPLINE_CURVE_WITH_KNOTS ( 'NONE', 3,
 ( #24133, #11029, #11190, #27022 ),
 .UNSPECIFIED., .F., .F.,
 ( 4, 4 ),
 ( 0.000000000000000000, 0.004600009204204574646 ),
 .UNSPECIFIED. ) ;
#22602=ORIENTED_EDGE ( 'NONE', *, *, #29527, .F. ) ;
#22635=LINE ( 'NONE', #4587, #16845 ) ;
#22645=DIRECTION ( 'NONE',  ( -1.000000000000000000, 0.000000000000000000, 0.000000000000000000 ) ) ;
#22698=ORIENTED_EDGE ( 'NONE', *, *, #28326, .F. ) ;
#22725=MECHANICAL_DESIGN_GEOMETRIC_PRESENTATION_REPRESENTATION('',(#9655),#3116);
#22744=CARTESIAN_POINT ( 'NONE',  ( -67.50000000000000000, 0.000000000000000000, 270.4495957273638282 ) ) ;
#22881=CARTESIAN_POINT ( 'NONE',  ( -67.50001199999999812, 142.1924241995298246, 11.23405475987244095 ) ) ;
#22900=EDGE_LOOP ( 'NONE', ( #9922, #7415, #29105, #5356, #16596, #20181, #23819 ) ) ;
#22917=DIRECTION ( 'NONE',  ( 0.000000000000000000, 0.000000000000000000, 1.000000000000000000 ) ) ;
#22984=CIRCLE ( 'NONE', #12108, 2.500000000000000000 ) ;
#23036=EDGE_LOOP ( 'NONE', ( #5882, #24627, #3217, #9246, #778, #29113 ) ) ;
#23050=CARTESIAN_POINT ( 'NONE',  ( -67.50001199999996970, 142.1924241995297677, -11.23405475987242674 ) ) ;
#23064=CARTESIAN_POINT ( 'NONE',  ( -59.75243488385262225, 194.9412087183787037, 2.169815710172075196 ) ) ;
#23080=DIRECTION ( 'NONE',  ( 0.000000000000000000, 0.000000000000000000, 1.000000000000000000 ) ) ;
#23163=VERTEX_POINT ( 'NONE', #14139 ) ;
#23194=ORIENTED_EDGE ( 'NONE', *, *, #7734, .F. ) ;
#23217=CARTESIAN_POINT ( 'NONE',  ( -67.50001199999998391, 137.9999999999999432, -1.112647398146382471 ) ) ;
#23228=EDGE_CURVE ( 'NONE', #26026, #28157, #9026, .T. ) ;
#23251=VERTEX_POINT ( 'NONE', #3908 ) ;
#23280=CARTESIAN_POINT ( 'NONE',  ( -67.50001199999999812, 171.1317437780265607, 5.477666192157153446 ) ) ;
#23292=EDGE_CURVE ( 'NONE', #23387, #22231, #16700, .T. ) ;
#23308=AXIS2_PLACEMENT_3D ( 'NONE', #2214, #7837, #15156 ) ;
#23319=AXIS2_PLACEMENT_3D ( 'NONE', #23440, #25997, #9997 ) ;
#23349=( LENGTH_UNIT ( ) NAMED_UNIT ( * ) SI_UNIT ( .MILLI., .METRE. ) );
#23387=VERTEX_POINT ( 'NONE', #25543 ) ;
#23406=CARTESIAN_POINT ( 'NONE',  ( -60.48814638060569848, 194.9711715815534205, -1.524404325634890700 ) ) ;
#23440=CARTESIAN_POINT ( 'NONE',  ( -60.00000000000000000, -7.347880794884118356E-15, 20.00000000000001776 ) ) ;
#23447=CARTESIAN_POINT ( 'NONE',  ( -67.50001199999999812, 167.8075758004702038, 11.23405475987244273 ) ) ;
#23467=ADVANCED_FACE ( 'NONE', ( #28096, #20435 ), #30831, .T. ) ;
#23476=CARTESIAN_POINT ( 'NONE',  ( -65.20000000000000284, -7.347880794884118356E-15, 19.29999999999998295 ) ) ;
#23498=CARTESIAN_POINT ( 'NONE',  ( -63.50000000000001421, 210.0000000000000000, 0.000000000000000000 ) ) ;
#23553=CARTESIAN_POINT ( 'NONE',  ( -67.50001199999996970, 141.4831703651135228, 10.36982646209945003 ) ) ;
#23557=EDGE_CURVE ( 'NONE', #17200, #8086, #1460, .T. ) ;
#23566=ADVANCED_FACE ( 'NONE', ( #29101 ), #28683, .T. ) ;
#23571=CARTESIAN_POINT ( 'NONE',  ( -60.98407617557292326, 194.9989950908677088, 0.3262505061364526227 ) ) ;
#23657=DIRECTION ( 'NONE',  ( -0.000000000000000000, 0.000000000000000000, -1.000000000000000000 ) ) ;
#23681=CARTESIAN_POINT ( 'NONE',  ( -56.61573505521625549, 194.9660755786677555, 1.651105572388385401 ) ) ;
#23802=DIRECTION ( 'NONE',  ( 0.000000000000000000, -1.000000000000000000, 0.000000000000000000 ) ) ;
#23819=ORIENTED_EDGE ( 'NONE', *, *, #30981, .F. ) ;
#23859=CIRCLE ( 'NONE', #21671, 4.199999999999988631 ) ;
#23909=ORIENTED_EDGE ( 'NONE', *, *, #32599, .T. ) ;
#23943=DIRECTION ( 'NONE',  ( 0.000000000000000000, -1.000000000000000000, 0.000000000000000000 ) ) ;
#23982=MANIFOLD_SOLID_BREP ( '\X2\00d8\X0\8.4 (8.4) Diameter Hole1', #17763 ) ;
#23990=VERTEX_POINT ( 'NONE', #8447 ) ;
#24014=CARTESIAN_POINT ( 'NONE',  ( 60.63708498984762940, 155.0000000000000000, -40.00000000000000000 ) ) ;
#24019=CARTESIAN_POINT ( 'NONE',  ( -67.50000000000000000, 155.0000000000000000, -37.00000000000000000 ) ) ;
#24056=PRODUCT_DEFINITION_FORMATION_WITH_SPECIFIED_SOURCE ( 'ANY', '', #16751, .NOT_KNOWN. ) ;
#24106=CARTESIAN_POINT ( 'NONE',  ( -58.50000000000002132, 209.9999999999999716, 0.000000000000000000 ) ) ;
#24116=ORIENTED_EDGE ( 'NONE', *, *, #7623, .T. ) ;
#24133=CARTESIAN_POINT ( 'NONE',  ( -67.50000000000000000, 122.1366465496900418, -17.00000000000001421 ) ) ;
#24152=VECTOR ( 'NONE', #31590, 1000.000000000000114 ) ;
#24187=LINE ( 'NONE', #13958, #14839 ) ;
#24208=ORIENTED_EDGE ( 'NONE', *, *, #27635, .F. ) ;
#24247=DIRECTION ( 'NONE',  ( -1.000000000000000000, 0.000000000000000000, 0.000000000000000000 ) ) ;
#24266=CARTESIAN_POINT ( 'NONE',  ( -67.50001199999998391, 166.2340547598724356, -12.80757580047018251 ) ) ;
#24343=DIRECTION ( 'NONE',  ( 0.000000000000000000, 0.000000000000000000, 1.000000000000000000 ) ) ;
#24369=AXIS2_PLACEMENT_3D ( 'NONE', #26835, #29567, #6220 ) ;
#24378=TOROIDAL_SURFACE ( 'NONE', #6407, 4.999999999999990230, 2.500000000000000000 ) ;
#24389=ADVANCED_FACE ( 'NONE', ( #9456 ), #19171, .T. ) ;
#24398=EDGE_CURVE ( 'NONE', #11008, #24997, #2083, .T. ) ;
#24402=LINE ( 'NONE', #29177, #28779 ) ;
#24426=LINE ( 'NONE', #21860, #24152 ) ;
#24485=ADVANCED_FACE ( 'NONE', ( #12182, #12349 ), #27841, .T. ) ;
#24517=DIRECTION ( 'NONE',  ( -1.000000000000000000, 0.000000000000000000, 0.000000000000000000 ) ) ;
#24568=CARTESIAN_POINT ( 'NONE',  ( -60.00000000000000000, -7.347880794884118356E-15, -20.00000000000001776 ) ) ;
#24581=ORIENTED_EDGE ( 'NONE', *, *, #8451, .T. ) ;
#24607=CIRCLE ( 'NONE', #28959, 2.499999999999988454 ) ;
#24612=CARTESIAN_POINT ( 'NONE',  ( -64.50000000000000000, -95.00000000000000000, 270.4495957273638282 ) ) ;
#24627=ORIENTED_EDGE ( 'NONE', *, *, #30981, .T. ) ;
#24683=LINE ( 'NONE', #11564, #15065 ) ;
#24732=CARTESIAN_POINT ( 'NONE',  ( -56.51255670714900248, 194.9711358487265613, -1.525379346234926992 ) ) ;
#24733=DIRECTION ( 'NONE',  ( 1.000000000000000000, 0.000000000000000000, 0.000000000000000000 ) ) ;
#24754=CARTESIAN_POINT ( 'NONE',  ( -52.50000000000002132, 155.0000000000000000, 6.938893903907228378E-15 ) ) ;
#24791=B_SPLINE_CURVE_WITH_KNOTS ( 'NONE', 3,
 ( #25664, #5387, #33675, #2677, #2332, #12720, #28395, #33501, #13057, #23447, #112, #10173, #10514, #23280, #279, #15772, #7952, #5053, #15444, #20894, #31291, #28728, #10674, #10349, #21053, #24266, #16099, #8441, #32109, #936, #29902, #3161, #14220, #774 ),
 .UNSPECIFIED., .F., .F.,
 ( 4, 2, 2, 2, 2, 2, 2, 2, 2, 2, 2, 2, 2, 2, 2, 2, 4 ),
 ( 0.000000000000000000, 0.03125000000000000000, 0.06250000000000000000, 0.09375000000000000000, 0.1250000000000000000, 0.1562500000000000000, 0.1875000000000000000, 0.2187500000000000000, 0.2500000000000000000, 0.2812500000000000000, 0.3125000000000000000, 0.3437500000000000000, 0.3750000000000000000, 0.4062500000000000000, 0.4375000000000000000, 0.4687500000000000000, 0.5000000000000000000 ),
 .UNSPECIFIED. ) ;
#24796=ADVANCED_FACE ( 'NONE', ( #13636 ), #29318, .F. ) ;
#24881=AXIS2_PLACEMENT_3D ( 'NONE', #17677, #2349, #33353 ) ;
#24900=CARTESIAN_POINT ( 'NONE',  ( -64.96121601855533356, -1.809269760319439646, -19.53878398144470907 ) ) ;
#24908=CARTESIAN_POINT ( 'NONE',  ( -54.79999999999999716, -6.711064459327494323E-15, -20.00000000000001776 ) ) ;
#24997=VERTEX_POINT ( 'NONE', #17540 ) ;
#25032=LINE ( 'NONE', #1684, #21200 ) ;
#25074=DIRECTION ( 'NONE',  ( 0.000000000000000000, 0.000000000000000000, 1.000000000000000000 ) ) ;
#25076=VERTEX_POINT ( 'NONE', #14987 ) ;
#25086=ORIENTED_EDGE ( 'NONE', *, *, #31667, .T. ) ;
#25201=ORIENTED_EDGE ( 'NONE', *, *, #29982, .T. ) ;
#25206=EDGE_CURVE ( 'NONE', #161, #747, #18951, .T. ) ;
#25219=CARTESIAN_POINT ( 'NONE',  ( -64.50000000000000000, -2.605762844159085212, -20.00000000000000000 ) ) ;
#25231=CARTESIAN_POINT ( 'NONE',  ( -56.07926260655170836, 194.9951118559247050, 0.6454098859825110335 ) ) ;
#25296=EDGE_CURVE ( 'NONE', #2428, #11008, #3165, .T. ) ;
#25316=LINE ( 'NONE', #30604, #8617 ) ;
#25338=CARTESIAN_POINT ( 'NONE',  ( -62.70000000000000284, -88.00000000000000000, 20.00000000000000000 ) ) ;
#25389=CARTESIAN_POINT ( 'NONE',  ( -67.50000000000000000, 155.0000000000000000, 6.938893903907228378E-15 ) ) ;
#25431=CARTESIAN_POINT ( 'NONE',  ( -67.50001199999999812, 139.7198396726429053, -7.533570508255913900 ) ) ;
#25475=CIRCLE ( 'NONE', #23319, 5.200000000000002842 ) ;
#25487=EDGE_CURVE ( 'NONE', #27043, #982, #23859, .T. ) ;
#25492=DIRECTION ( 'NONE',  ( -1.000000000000000000, 0.000000000000000000, 0.000000000000000000 ) ) ;
#25504=B_SPLINE_CURVE_WITH_KNOTS ( 'NONE', 3,
 ( #28338, #28506, #17948, #33444, #10453, #17766, #20827, #33613, #10620, #23050, #31066, #31232, #25431, #2613, #10115, #17598, #23217, #28664, #12492, #28163, #7724, #4820, #25605, #23553, #22881, #25775, #20494, #30726, #5323, #4994, #33272, #15381, #30897, #2270 ),
 .UNSPECIFIED., .F., .F.,
 ( 4, 2, 2, 2, 2, 2, 2, 2, 2, 2, 2, 2, 2, 2, 2, 2, 4 ),
 ( 0.5000000000000000000, 0.5312500000000000000, 0.5625000000000000000, 0.5937500000000001110, 0.6250000000000001110, 0.6562500000000001110, 0.6875000000000002220, 0.7187500000000002220, 0.7500000000000002220, 0.7812500000000002220, 0.8125000000000002220, 0.8437500000000001110, 0.8750000000000001110, 0.9062500000000000000, 0.9375000000000000000, 0.9687500000000000000, 1.000000000000000000 ),
 .UNSPECIFIED. ) ;
#25505=EDGE_LOOP ( 'NONE', ( #10997, #8002, #14509, #6480 ) ) ;
#25543=CARTESIAN_POINT ( 'NONE',  ( -54.30000000000001847, -88.00000000000000000, -20.00000000000000000 ) ) ;
#25565=FACE_OUTER_BOUND ( 'NONE', #15450, .T. ) ;
#25590=ORIENTED_EDGE ( 'NONE', *, *, #16647, .F. ) ;
#25598=ORIENTED_EDGE ( 'NONE', *, *, #17095, .F. ) ;
#25605=CARTESIAN_POINT ( 'NONE',  ( -67.50001199999998391, 140.2468628165998439, 8.519561460567032896 ) ) ;
#25607=CARTESIAN_POINT ( 'NONE',  ( -63.49999999999884892, 212.5000000000003695, -3.061616997868142046E-16 ) ) ;
#25664=CARTESIAN_POINT ( 'NONE',  ( -67.50000599999999906, 155.0000000000000000, 17.00000000000001421 ) ) ;
#25683=VERTEX_POINT ( 'NONE', #1829 ) ;
#25713=EDGE_LOOP ( 'NONE', ( #24581, #31169, #10305, #28948 ) ) ;
#25775=CARTESIAN_POINT ( 'NONE',  ( -67.50001199999998391, 143.7659452401275928, 12.80757580047018962 ) ) ;
#25793=CARTESIAN_POINT ( 'NONE',  ( -59.60814253741918378, 194.9368883388851259, -2.246975524854183170 ) ) ;
#25847=ORIENTED_EDGE ( 'NONE', *, *, #29775, .T. ) ;
#25867=DIRECTION ( 'NONE',  ( -1.000000000000000000, 0.000000000000000000, 0.000000000000000000 ) ) ;
#25912=DIRECTION ( 'NONE',  ( -1.000000000000000000, -0.000000000000000000, -0.000000000000000000 ) ) ;
#25958=AXIS2_PLACEMENT_3D ( 'NONE', #488, #816, #10886 ) ;
#25997=DIRECTION ( 'NONE',  ( -0.000000000000000000, -0.000000000000000000, -1.000000000000000000 ) ) ;
#26026=VERTEX_POINT ( 'NONE', #5557 ) ;
#26226=DIRECTION ( 'NONE',  ( 0.000000000000000000, 0.000000000000000000, 1.000000000000000000 ) ) ;
#26229=SHAPE_DEFINITION_REPRESENTATION ( #6421, #30038 ) ;
#26246=EDGE_LOOP ( 'NONE', ( #5833, #10775 ) ) ;
#26269=PLANE ( 'NONE',  #8293 ) ;
#26311=CARTESIAN_POINT ( 'NONE',  ( -63.50000000000004263, 215.0000000000000000, 0.000000000000000000 ) ) ;
#26340=ORIENTED_EDGE ( 'NONE', *, *, #13929, .T. ) ;
#26488=CIRCLE ( 'NONE', #13993, 37.00000000000000711 ) ;
#26499=PRESENTATION_STYLE_ASSIGNMENT (( #5717 ) ) ;
#26595=VECTOR ( 'NONE', #12166, 1000.000000000000000 ) ;
#26607=CARTESIAN_POINT ( 'NONE',  ( -52.50000000000002132, 120.3589838486224437, 20.00000000000000000 ) ) ;
#26634=ORIENTED_EDGE ( 'NONE', *, *, #25296, .T. ) ;
#26635=LINE ( 'NONE', #3137, #16690 ) ;
#26654=ORIENTED_EDGE ( 'NONE', *, *, #31667, .F. ) ;
#26662=EDGE_CURVE ( 'NONE', #32153, #14133, #26488, .T. ) ;
#26667=( NAMED_UNIT ( * ) PLANE_ANGLE_UNIT ( ) SI_UNIT ( $, .RADIAN. ) );
#26677=AXIS2_PLACEMENT_3D ( 'NONE', #10085, #5774, #24343 ) ;
#26712=CARTESIAN_POINT ( 'NONE',  ( -63.49999999999884892, 217.5000000000001990, 0.000000000000000000 ) ) ;
#26742=DIRECTION ( 'NONE',  ( 1.000000000000000000, 0.000000000000000000, 0.000000000000000000 ) ) ;
#26783=AXIS2_PLACEMENT_3D ( 'NONE', #8384, #13321, #3257 ) ;
#26809=LINE ( 'NONE', #3813, #18383 ) ;
#26835=CARTESIAN_POINT ( 'NONE',  ( -63.49999999999884892, 215.0000000000003979, 0.000000000000000000 ) ) ;
#26906=DIRECTION ( 'NONE',  ( 1.000000000000000000, 0.000000000000000000, 0.000000000000000000 ) ) ;
#26915=ORIENTED_EDGE ( 'NONE', *, *, #6806, .T. ) ;
#26923=ORIENTED_EDGE ( 'NONE', *, *, #19325, .F. ) ;
#26948=EDGE_CURVE ( 'NONE', #33071, #18396, #26635, .T. ) ;
#26962=DIRECTION ( 'NONE',  ( -1.000000000000000000, 0.000000000000000000, 0.000000000000000000 ) ) ;
#26988=VECTOR ( 'NONE', #6542, 1000.000000000000000 ) ;
#27006=EDGE_CURVE ( 'NONE', #19514, #22398, #24683, .T. ) ;
#27022=CARTESIAN_POINT ( 'NONE',  ( -64.50000000000000000, 120.3589838486224579, -20.00000000000000000 ) ) ;
#27043=VERTEX_POINT ( 'NONE', #15256 ) ;
#27059=DIRECTION ( 'NONE',  ( 0.000000000000000000, 1.000000000000000000, 0.000000000000000000 ) ) ;
#27096=AXIS2_PLACEMENT_3D ( 'NONE', #623, #15955, #5891 ) ;
#27131=ORIENTED_EDGE ( 'NONE', *, *, #8963, .F. ) ;
#27178=ORIENTED_EDGE ( 'NONE', *, *, #29115, .T. ) ;
#27217=ADVANCED_FACE ( 'NONE', ( #31436 ), #28710, .T. ) ;
#27293=CARTESIAN_POINT ( 'NONE',  ( -67.50000000000000000, 155.0000000000000000, 6.938893903907228378E-15 ) ) ;
#27356=AXIS2_PLACEMENT_3D ( 'NONE', #6974, #3897, #9349 ) ;
#27468=LINE ( 'NONE', #17754, #21391 ) ;
#27475=ORIENTED_EDGE ( 'NONE', *, *, #8139, .F. ) ;
#27511=EDGE_CURVE ( 'NONE', #3377, #25076, #26809, .T. ) ;
#27553=CIRCLE ( 'NONE', #15042, 5.200000000000009948 ) ;
#27555=DIRECTION ( 'NONE',  ( 0.7071067811865454633, -0.000000000000000000, 0.7071067811865495711 ) ) ;
#27569=AXIS2_PLACEMENT_3D ( 'NONE', #7496, #15316, #23657 ) ;
#27584=ORIENTED_EDGE ( 'NONE', *, *, #27635, .T. ) ;
#27608=CARTESIAN_POINT ( 'NONE',  ( -56.12844631811822893, 194.9921284422999292, -0.8077925457893648797 ) ) ;
#27627=CARTESIAN_POINT ( 'NONE',  ( -58.50000000000002132, 209.9999999999999716, -2.500000000000000000 ) ) ;
#27635=EDGE_CURVE ( 'NONE', #22398, #20653, #33452, .T. ) ;
#27657=CIRCLE ( 'NONE', #10800, 40.00000000000000711 ) ;
#27780=CARTESIAN_POINT ( 'NONE',  ( -55.99986651211894184, 195.0000083429897586, 0.1629166443388770646 ) ) ;
#27841=PLANE ( 'NONE',  #31971 ) ;
#27919=VERTEX_POINT ( 'NONE', #5331 ) ;
#27961=DIRECTION ( 'NONE',  ( -1.000000000000000000, -0.000000000000000000, 0.000000000000000000 ) ) ;
#27971=ORIENTED_EDGE ( 'NONE', *, *, #24398, .F. ) ;
#28012=LINE ( 'NONE', #4678, #9631 ) ;
#28096=FACE_BOUND ( 'NONE', #16815, .T. ) ;
#28109=VERTEX_POINT ( 'NONE', #31886 ) ;
#28156=VECTOR ( 'NONE', #32937, 1000.000000000000000 ) ;
#28157=VERTEX_POINT ( 'NONE', #26607 ) ;
#28163=CARTESIAN_POINT ( 'NONE',  ( -67.50001199999996970, 138.5437169723398085, 4.407803664655115305 ) ) ;
#28167=( BOUNDED_CURVE ( )  B_SPLINE_CURVE ( 3, ( #3945, #24900, #14840, #14344 ),
 .UNSPECIFIED., .F., .T. ) 
 B_SPLINE_CURVE_WITH_KNOTS ( ( 4, 4 ),
 ( 2.616713720088120532, 3.141592653589793116 ),
 .UNSPECIFIED. ) 
 CURVE ( )  GEOMETRIC_REPRESENTATION_ITEM ( )  RATIONAL_B_SPLINE_CURVE ( ( 1.000000000000000000, 0.9771733092046011038, 0.9771733092046011038, 1.000000000000000000 ) ) 
 REPRESENTATION_ITEM ( '' )  );
#28175=AXIS2_PLACEMENT_3D ( 'NONE', #29399, #6047, #16439 ) ;
#28179=ORIENTED_EDGE ( 'NONE', *, *, #30113, .F. ) ;
#28184=VECTOR ( 'NONE', #9390, 1000.000000000000000 ) ;
#28231=VECTOR ( 'NONE', #22172, 1000.000000000000000 ) ;
#28280=ORIENTED_EDGE ( 'NONE', *, *, #27511, .F. ) ;
#28326=EDGE_CURVE ( 'NONE', #12982, #3377, #9229, .T. ) ;
#28338=CARTESIAN_POINT ( 'NONE',  ( -67.50000599999999906, 155.0000000000000000, -17.00000000000000711 ) ) ;
#28352=CARTESIAN_POINT ( 'NONE',  ( -58.66522414286995968, 194.9217985566782545, 2.500000000000000444 ) ) ;
#28395=CARTESIAN_POINT ( 'NONE',  ( -67.50001199999999812, 163.5195614605670755, 14.75313718340012414 ) ) ;
#28481=EDGE_LOOP ( 'NONE', ( #18550, #17749, #13266, #31095 ) ) ;
#28506=CARTESIAN_POINT ( 'NONE',  ( -67.50001200000001234, 153.8873526018536779, -17.00000000000000711 ) ) ;
#28522=CARTESIAN_POINT ( 'NONE',  ( -60.74722861894645831, 194.9849492171461804, 1.107464383744043657 ) ) ;
#28622=CARTESIAN_POINT ( 'NONE',  ( -64.50000000000000000, 0.000000000000000000, -20.00000000000000000 ) ) ;
#28651=ADVANCED_FACE ( 'NONE', ( #28805 ), #24378, .T. ) ;
#28664=CARTESIAN_POINT ( 'NONE',  ( -67.50001199999998391, 137.9999999999999432, 1.112647398146386912 ) ) ;
#28677=CARTESIAN_POINT ( 'NONE',  ( -59.60884549136632415, 194.9369081818307166, 2.246623501397673639 ) ) ;
#28683=CONICAL_SURFACE ( 'NONE', #13979, 37.00000000000000711, 0.7853981633974482790 ) ;
#28710=PLANE ( 'NONE',  #11302 ) ;
#28728=CARTESIAN_POINT ( 'NONE',  ( -67.50001199999998391, 170.2801603273571800, -7.533570508255905018 ) ) ;
#28764=EDGE_CURVE ( 'NONE', #17200, #20297, #29296, .T. ) ;
#28779=VECTOR ( 'NONE', #1067, 1000.000000000000114 ) ;
#28805=FACE_OUTER_BOUND ( 'NONE', #7630, .T. ) ;
#28822=ORIENTED_EDGE ( 'NONE', *, *, #8909, .T. ) ;
#28872=EDGE_CURVE ( 'NONE', #747, #2428, #17305, .T. ) ;
#28948=ORIENTED_EDGE ( 'NONE', *, *, #23228, .T. ) ;
#28959=AXIS2_PLACEMENT_3D ( 'NONE', #9817, #12197, #20198 ) ;
#29017=ORIENTED_EDGE ( 'NONE', *, *, #30996, .F. ) ;
#29034=AXIS2_PLACEMENT_3D ( 'NONE', #25389, #30687, #12451 ) ;
#29075=FACE_BOUND ( 'NONE', #16356, .T. ) ;
#29101=FACE_OUTER_BOUND ( 'NONE', #28481, .T. ) ;
#29105=ORIENTED_EDGE ( 'NONE', *, *, #29742, .T. ) ;
#29113=ORIENTED_EDGE ( 'NONE', *, *, #29775, .F. ) ;
#29115=EDGE_CURVE ( 'NONE', #2428, #16283, #4233, .T. ) ;
#29130=ADVANCED_FACE ( 'NONE', ( #29803 ), #6464, .F. ) ;
#29177=CARTESIAN_POINT ( 'NONE',  ( -96.16666666666678509, -63.33333333333321491, 11.66666666666661278 ) ) ;
#29228=SURFACE_STYLE_FILL_AREA ( #11009 ) ;
#29231=ORIENTED_EDGE ( 'NONE', *, *, #27511, .T. ) ;
#29236=VECTOR ( 'NONE', #14951, 1000.000000000000000 ) ;
#29240=PLANE ( 'NONE',  #27096 ) ;
#29296=LINE ( 'NONE', #24014, #18405 ) ;
#29318=CYLINDRICAL_SURFACE ( 'NONE', #33076, 5.200000000000009948 ) ;
#29357=CIRCLE ( 'NONE', #17939, 40.00000000000000711 ) ;
#29359=ORIENTED_EDGE ( 'NONE', *, *, #30996, .T. ) ;
#29399=CARTESIAN_POINT ( 'NONE',  ( 60.63708498984762940, 155.0000000000000000, 6.938893903907228378E-15 ) ) ;
#29527=EDGE_CURVE ( 'NONE', #26026, #23251, #6756, .T. ) ;
#29541=CIRCLE ( 'NONE', #8343, 2.500000000000000000 ) ;
#29567=DIRECTION ( 'NONE',  ( 1.000000000000000000, 0.000000000000000000, 0.000000000000000000 ) ) ;
#29652=DIRECTION ( 'NONE',  ( -1.000000000000000000, 0.000000000000000000, 0.000000000000000000 ) ) ;
#29710=ORIENTED_EDGE ( 'NONE', *, *, #26948, .F. ) ;
#29742=EDGE_CURVE ( 'NONE', #23251, #23990, #25475, .T. ) ;
#29747=EDGE_CURVE ( 'NONE', #28109, #6207, #25316, .T. ) ;
#29775=EDGE_CURVE ( 'NONE', #33083, #17200, #27657, .T. ) ;
#29780=PRODUCT_DEFINITION ( 'UNKNOWN', '', #24056, #21687 ) ;
#29803=FACE_OUTER_BOUND ( 'NONE', #32189, .T. ) ;
#29818=EDGE_LOOP ( 'NONE', ( #12802, #32321, #11165, #4202 ) ) ;
#29872=ORIENTED_EDGE ( 'NONE', *, *, #30113, .T. ) ;
#29897=DIRECTION ( 'NONE',  ( -1.000000000000000000, 0.000000000000000000, 0.000000000000000000 ) ) ;
#29902=CARTESIAN_POINT ( 'NONE',  ( -67.50001199999999812, 159.4078036646551482, -16.45628302766012752 ) ) ;
#29915=AXIS2_PLACEMENT_3D ( 'NONE', #22128, #9521, #17187 ) ;
#29969=CARTESIAN_POINT ( 'NONE',  ( -63.50000000000004263, 215.0000000000000000, 2.500000000000000000 ) ) ;
#29982=EDGE_CURVE ( 'NONE', #1081, #18384, #5703, .T. ) ;
#29990=CARTESIAN_POINT ( 'NONE',  ( -54.79999999999999716, -6.711064459327494323E-15, 270.4495957273638282 ) ) ;
#30023=AXIS2_PLACEMENT_3D ( 'NONE', #1717, #24733, #33239 ) ;
#30036=DIRECTION ( 'NONE',  ( 0.000000000000000000, -1.000000000000000000, 0.000000000000000000 ) ) ;
#30038=SHAPE_REPRESENTATION ( 'pad arm right_right', ( #2404 ), #31228 ) ;
#30051=CARTESIAN_POINT ( 'NONE',  ( -64.50000000000000000, 0.000000000000000000, 20.00000000000000000 ) ) ;
#30113=EDGE_CURVE ( 'NONE', #22576, #9805, #5909, .T. ) ;
#30198=CARTESIAN_POINT ( 'NONE',  ( -67.50000000000000000, 0.000000000000000000, -17.00000000000001421 ) ) ;
#30203=DIRECTION ( 'NONE',  ( 0.000000000000000000, 0.000000000000000000, 1.000000000000000000 ) ) ;
#30246=ORIENTED_EDGE ( 'NONE', *, *, #6390, .T. ) ;
#30249=CARTESIAN_POINT ( 'NONE',  ( -52.50000000000002132, 155.0000000000000000, -16.99999999999999645 ) ) ;
#30286=AXIS2_PLACEMENT_3D ( 'NONE', #16493, #11397, #32164 ) ;
#30345=CARTESIAN_POINT ( 'NONE',  ( -57.24307706584514932, 194.9404480003898925, -2.185445380844633689 ) ) ;
#30377=ORIENTED_EDGE ( 'NONE', *, *, #32599, .F. ) ;
#30404=VERTEX_POINT ( 'NONE', #15521 ) ;
#30411=DIRECTION ( 'NONE',  ( 0.000000000000000000, 0.000000000000000000, 1.000000000000000000 ) ) ;
#30451=ORIENTED_EDGE ( 'NONE', *, *, #33516, .T. ) ;
#30512=CARTESIAN_POINT ( 'NONE',  ( -56.32919368135717519, 194.9806731544236982, 1.250698461946182505 ) ) ;
#30562=ORIENTED_EDGE ( 'NONE', *, *, #18354, .T. ) ;
#30563=CARTESIAN_POINT ( 'NONE',  ( -58.82891977373553516, 194.9228321189716837, -2.483646737656201253 ) ) ;
#30604=CARTESIAN_POINT ( 'NONE',  ( -67.50000000000000000, 155.0000000000000000, 37.00000000000001421 ) ) ;
#30646=CARTESIAN_POINT ( 'NONE',  ( -65.20000000000000284, 0.9203920079924619024, 19.30000000000001847 ) ) ;
#30682=( NAMED_UNIT ( * ) PLANE_ANGLE_UNIT ( ) SI_UNIT ( $, .RADIAN. ) );
#30687=DIRECTION ( 'NONE',  ( 1.000000000000000000, 0.000000000000000000, 0.000000000000000000 ) ) ;
#30726=CARTESIAN_POINT ( 'NONE',  ( -67.50001199999996970, 146.4804385394329245, 14.75313718340011881 ) ) ;
#30740=CARTESIAN_POINT ( 'NONE',  ( -60.66959905230670103, 194.9806057094332346, 1.252942659870247555 ) ) ;
#30761=ADVANCED_FACE ( 'NONE', ( #14530 ), #32591, .F. ) ;
#30831=PLANE ( 'NONE',  #27569 ) ;
#30897=CARTESIAN_POINT ( 'NONE',  ( -67.50001199999998391, 153.8873526018535927, 17.00000000000001066 ) ) ;
#30911=CARTESIAN_POINT ( 'NONE',  ( -60.98379214578430663, 194.9989775857802385, -0.3278793750673599239 ) ) ;
#30981=EDGE_CURVE ( 'NONE', #28157, #12982, #12999, .T. ) ;
#30996=EDGE_CURVE ( 'NONE', #18396, #30404, #25504, .T. ) ;
#31022=FILL_AREA_STYLE_COLOUR ( '', #22505 ) ;
#31066=CARTESIAN_POINT ( 'NONE',  ( -67.50001199999999812, 141.4831703651136081, -10.36982646209944470 ) ) ;
#31095=ORIENTED_EDGE ( 'NONE', *, *, #13935, .F. ) ;
#31110=CARTESIAN_POINT ( 'NONE',  ( -65.20000000000000284, 0.9203920079924583497, -19.30000000000004690 ) ) ;
#31169=ORIENTED_EDGE ( 'NONE', *, *, #2461, .T. ) ;
#31178=FILL_AREA_STYLE ('',( #31022 ) ) ;
#31228=( GEOMETRIC_REPRESENTATION_CONTEXT ( 3 ) GLOBAL_UNCERTAINTY_ASSIGNED_CONTEXT ( ( #31469 ) ) GLOBAL_UNIT_ASSIGNED_CONTEXT ( ( #23349, #10246, #33050 ) ) REPRESENTATION_CONTEXT ( 'NONE', 'WORKASPACE' ) );
#31230=ADVANCED_FACE ( 'NONE', ( #3883 ), #9616, .T. ) ;
#31232=CARTESIAN_POINT ( 'NONE',  ( -67.50001199999996970, 140.2468628165999007, -8.519561460567018685 ) ) ;
#31291=CARTESIAN_POINT ( 'NONE',  ( -67.50001199999999812, 171.1317437780266459, -5.477666192157138347 ) ) ;
#31362=AXIS2_PLACEMENT_3D ( 'NONE', #1598, #21866, #4145 ) ;
#31408=AXIS2_PLACEMENT_3D ( 'NONE', #9101, #29897, #19100 ) ;
#31436=FACE_OUTER_BOUND ( 'NONE', #15567, .T. ) ;
#31440=AXIS2_PLACEMENT_3D ( 'NONE', #32349, #26906, #16013 ) ;
#31457=ADVANCED_FACE ( 'NONE', ( #7125 ), #33188, .F. ) ;
#31469=UNCERTAINTY_MEASURE_WITH_UNIT (LENGTH_MEASURE( 1.000000000000000082E-05 ), #23349, 'distance_accuracy_value', 'NONE');
#31550=CARTESIAN_POINT ( 'NONE',  ( -67.50000000000000000, 0.000000000000000000, 17.00000000000001421 ) ) ;
#31590=DIRECTION ( 'NONE',  ( 0.7071067811865474617, 0.000000000000000000, -0.7071067811865474617 ) ) ;
#31630=FACE_OUTER_BOUND ( 'NONE', #22900, .T. ) ;
#31654=CARTESIAN_POINT ( 'NONE',  ( -67.50000000000000000, 155.0000000000000000, 6.938893903907228378E-15 ) ) ;
#31667=EDGE_CURVE ( 'NONE', #27919, #22576, #27553, .T. ) ;
#31828=EDGE_LOOP ( 'NONE', ( #9095, #7380, #11745, #3968 ) ) ;
#31830=( BOUNDED_CURVE ( )  B_SPLINE_CURVE ( 3, ( #33489, #31110, #12874, #13046 ),
 .UNSPECIFIED., .F., .F. ) 
 B_SPLINE_CURVE_WITH_KNOTS ( ( 4, 4 ),
 ( 3.141592653589793116, 3.666471587091465700 ),
 .UNSPECIFIED. ) 
 CURVE ( )  GEOMETRIC_REPRESENTATION_ITEM ( )  RATIONAL_B_SPLINE_CURVE ( ( 1.000000000000000000, 0.9771733092046011038, 0.9771733092046011038, 1.000000000000000000 ) ) 
 REPRESENTATION_ITEM ( '' )  );
#31886=CARTESIAN_POINT ( 'NONE',  ( -67.50000000000000000, 155.0000000000000000, 37.00000000000001421 ) ) ;
#31931=EDGE_LOOP ( 'NONE', ( #29231, #33437, #28179, #26654, #3662, #16201, #28822 ) ) ;
#31971=AXIS2_PLACEMENT_3D ( 'NONE', #22744, #5477, #23080 ) ;
#32026=VECTOR ( 'NONE', #32466, 1000.000000000000000 ) ;
#32080=ORIENTED_EDGE ( 'NONE', *, *, #19116, .F. ) ;
#32091=EDGE_CURVE ( 'NONE', #10396, #30404, #24187, .T. ) ;
#32109=CARTESIAN_POINT ( 'NONE',  ( -67.50001199999999812, 162.5335705082559059, -15.28016032735712493 ) ) ;
#32119=ORIENTED_EDGE ( 'NONE', *, *, #16647, .T. ) ;
#32153=VERTEX_POINT ( 'NONE', #24019 ) ;
#32164=DIRECTION ( 'NONE',  ( 0.000000000000000000, 0.000000000000000000, -1.000000000000000000 ) ) ;
#32189=EDGE_LOOP ( 'NONE', ( #25590, #15416 ) ) ;
#32207=DIRECTION ( 'NONE',  ( 0.000000000000000000, 1.000000000000000000, -0.000000000000000000 ) ) ;
#32298=( GEOMETRIC_REPRESENTATION_CONTEXT ( 3 ) GLOBAL_UNCERTAINTY_ASSIGNED_CONTEXT ( ( #13391 ) ) GLOBAL_UNIT_ASSIGNED_CONTEXT ( ( #17898, #30682, #7848 ) ) REPRESENTATION_CONTEXT ( 'NONE', 'WORKASPACE' ) );
#32305=AXIS2_PLACEMENT_3D ( 'NONE', #143, #15131, #33369 ) ;
#32321=ORIENTED_EDGE ( 'NONE', *, *, #19350, .T. ) ;
#32349=CARTESIAN_POINT ( 'NONE',  ( -63.49999999999884892, 215.0000000000003979, 0.000000000000000000 ) ) ;
#32394=DIRECTION ( 'NONE',  ( -1.000000000000000000, 0.000000000000000000, 0.000000000000000000 ) ) ;
#32434=CYLINDRICAL_SURFACE ( 'NONE', #31408, 40.00000000000000711 ) ;
#32466=DIRECTION ( 'NONE',  ( 0.000000000000000000, 0.000000000000000000, 1.000000000000000000 ) ) ;
#32532=LINE ( 'NONE', #29990, #17632 ) ;
#32577=ORIENTED_EDGE ( 'NONE', *, *, #26948, .T. ) ;
#32591=CYLINDRICAL_SURFACE ( 'NONE', #9206, 17.00000000000000355 ) ;
#32599=EDGE_CURVE ( 'NONE', #25683, #20297, #8331, .T. ) ;
#32745=CYLINDRICAL_SURFACE ( 'NONE', #31362, 5.200000000000009948 ) ;
#32937=DIRECTION ( 'NONE',  ( 0.000000000000000000, 1.000000000000000000, 0.000000000000000000 ) ) ;
#32942=ORIENTED_EDGE ( 'NONE', *, *, #16858, .T. ) ;
#33047=EDGE_LOOP ( 'NONE', ( #29710, #10230, #7906, #7593 ) ) ;
#33050=( NAMED_UNIT ( * ) SI_UNIT ( $, .STERADIAN. ) SOLID_ANGLE_UNIT ( ) );
#33060=CARTESIAN_POINT ( 'NONE',  ( -58.50000000000002132, 194.9217985566782829, -2.500000000000000000 ) ) ;
#33071=VERTEX_POINT ( 'NONE', #30249 ) ;
#33076=AXIS2_PLACEMENT_3D ( 'NONE', #16354, #18596, #29652 ) ;
#33083=VERTEX_POINT ( 'NONE', #16953 ) ;
#33096=DIRECTION ( 'NONE',  ( 0.000000000000000000, 0.000000000000000000, -1.000000000000000000 ) ) ;
#33174=ORIENTED_EDGE ( 'NONE', *, *, #3963, .T. ) ;
#33188=PLANE ( 'NONE',  #19388 ) ;
#33239=DIRECTION ( 'NONE',  ( 0.000000000000000000, 0.000000000000000000, -1.000000000000000000 ) ) ;
#33272=CARTESIAN_POINT ( 'NONE',  ( -67.50001199999998391, 150.5921963353448803, 16.45628302766014173 ) ) ;
#33300=DIRECTION ( 'NONE',  ( -1.000000000000000000, 0.000000000000000000, 0.000000000000000000 ) ) ;
#33306=ORIENTED_EDGE ( 'NONE', *, *, #27006, .F. ) ;
#33348=ORIENTED_EDGE ( 'NONE', *, *, #6390, .F. ) ;
#33353=DIRECTION ( 'NONE',  ( -1.000000000000000000, 0.000000000000000000, 0.000000000000000000 ) ) ;
#33369=DIRECTION ( 'NONE',  ( -1.000000000000000000, 0.000000000000000000, -0.000000000000000000 ) ) ;
#33373=VECTOR ( 'NONE', #11678, 1000.000000000000000 ) ;
#33385=ORIENTED_EDGE ( 'NONE', *, *, #7035, .F. ) ;
#33437=ORIENTED_EDGE ( 'NONE', *, *, #9924, .T. ) ;
#33444=CARTESIAN_POINT ( 'NONE',  ( -67.50001199999999812, 150.5921963353448803, -16.45628302766012752 ) ) ;
#33452=LINE ( 'NONE', #20333, #28156 ) ;
#33456=CARTESIAN_POINT ( 'NONE',  ( -60.15281075484971041, 194.9558321103198466, 1.882765505879504309 ) ) ;
#33480=ADVANCED_FACE ( 'NONE', ( #16079 ), #6192, .T. ) ;
#33489=CARTESIAN_POINT ( 'NONE',  ( -65.20000000000000284, -7.347880794884118356E-15, -19.30000000000003979 ) ) ;
#33501=CARTESIAN_POINT ( 'NONE',  ( -67.50001199999999812, 165.3698264620994394, 13.51682963488644162 ) ) ;
#33516=EDGE_CURVE ( 'NONE', #32153, #20297, #24426, .T. ) ;
#33517=CARTESIAN_POINT ( 'NONE',  ( -65.20000000000000284, -7.347880794884118356E-15, 19.29999999999998295 ) ) ;
#33596=VECTOR ( 'NONE', #329, 1000.000000000000000 ) ;
#33613=CARTESIAN_POINT ( 'NONE',  ( -67.50001199999998391, 144.6301735379005322, -13.51682963488642564 ) ) ;
#33653=VECTOR ( 'NONE', #12030, 1000.000000000000000 ) ;
#33667=CIRCLE ( 'NONE', #5896, 2.500000000000000000 ) ;
#33675=CARTESIAN_POINT ( 'NONE',  ( -67.50001200000001234, 157.2252672838932597, 16.89041650604972133 ) ) ;
ENDSEC;
END-ISO-10303-21;
